ISO-10303-21;
HEADER;
FILE_DESCRIPTION (('STEP AP214'),
    '1' );
FILE_NAME ('8. Bar.step',
    '2026-10-09T14:04:53',
    ( '' ),
    ( '' ),
    'SwSTEP 2.0',
    'SolidWorks 2021',
    '' );
FILE_SCHEMA (( 'AUTOMOTIVE_DESIGN' ));
ENDSEC;

DATA;
#1=VERTEX_POINT ( 'NONE', #17992 ) ;
#8=B_SPLINE_CURVE_WITH_KNOTS ( 'NONE', 3,
 ( #50184, #49649, #7583, #83088, #90116, #41565, #65840, #73380, #17841, #66367, #58829, #99249, #42622, #9178, #75522, #16219, #8125, #82557, #34041, #42089, #34577, #90651, #50690, #83607, #1616, #67451, #23829, #56671, #48578, #41038, #106277, #32440, #98201, #49106, #57729, #82005 ),
 .UNSPECIFIED., .F., .F.,
 ( 4, 2, 2, 2, 2, 2, 2, 2, 2, 2, 2, 2, 2, 2, 2, 2, 2, 4 ),
 ( 0.000000000000000000, 0.0008074604767267243646, 0.001614920953453448729, 0.002422381430180173094, 0.003229841906906897459, 0.004037302383633621823, 0.004844762860360346188, 0.005652223337087070552, 0.006459683813813794917, 0.007267144290540519282, 0.008074604767267243646, 0.008882065243993968878, 0.009689525720720692376, 0.01049698619744741587, 0.01130444667417414110, 0.01211190715090086634, 0.01251563738926422809, 0.01291936762762758983 ),
 .UNSPECIFIED. ) ;
#29=CARTESIAN_POINT ( 'NONE',  ( -7.896254658894419798, -61.21070817245801976, 1.307282859663299268 ) ) ;
#79=CARTESIAN_POINT ( 'NONE',  ( 4.595881407952572495, -86.06625433201324427, -3.857520671226066789 ) ) ;
#233=EDGE_CURVE ( 'NONE', #104211, #1, #64264, .T. ) ;
#246=CARTESIAN_POINT ( 'NONE',  ( 9.333555687487635311, 248.2189730339102027, 3.591168747312695420 ) ) ;
#283=CARTESIAN_POINT ( 'NONE',  ( -7.344133061198927948, -82.55505607319420847, 3.176267128233875248 ) ) ;
#290=CARTESIAN_POINT ( 'NONE',  ( -9.699189539447148789, 253.1769222824670180, -2.444343703917194688 ) ) ;
#392=CARTESIAN_POINT ( 'NONE',  ( 4.472135954999578722, -84.72588149001676072, -4.000000000000003553 ) ) ;
#406=ORIENTED_EDGE ( 'NONE', *, *, #769, .T. ) ;
#429=DIRECTION ( 'NONE',  ( 1.000000000000000000, -0.000000000000000000, -0.000000000000000000 ) ) ;
#458=ORIENTED_EDGE ( 'NONE', *, *, #93604, .T. ) ;
#553=CARTESIAN_POINT ( 'NONE',  ( -7.344133061198929724, -62.55505607319423689, 3.176267128233876136 ) ) ;
#769=EDGE_CURVE ( 'NONE', #67191, #31789, #46307, .T. ) ;
#821=CARTESIAN_POINT ( 'NONE',  ( -9.482993638194566088, 252.4434872025367440, -3.177441187500450681 ) ) ;
#880=( GEOMETRIC_REPRESENTATION_CONTEXT ( 3 ) GLOBAL_UNCERTAINTY_ASSIGNED_CONTEXT ( ( #60618 ) ) GLOBAL_UNIT_ASSIGNED_CONTEXT ( ( #97027, #23168, #81358 ) ) REPRESENTATION_CONTEXT ( 'NONE', 'WORKASPACE' ) );
#919=CARTESIAN_POINT ( 'NONE',  ( 4.903871675326606727, -82.97914192698505076, -3.461400506969855684 ) ) ;
#944=AXIS2_PLACEMENT_3D ( 'NONE', #49176, #25494, #74522 ) ;
#1059=B_SPLINE_CURVE_WITH_KNOTS ( 'NONE', 3,
 ( #76944, #85592, #59182, #69402, #18750, #91551, #9537, #93135, #28431, #42448, #27386, #75338, #17659, #50522, #11127, #42994, #1440, #34402, #44055, #67277, #93674, #76400, #34928, #100156, #36006, #26322, #92061, #2514, #19826, #18203, #67795, #100681, #68879, #101753, #35462, #26848 ),
 .UNSPECIFIED., .F., .F.,
 ( 4, 2, 2, 2, 2, 2, 2, 2, 2, 2, 2, 2, 2, 2, 2, 2, 2, 4 ),
 ( 0.000000000000000000, 0.0008074604767267251236, 0.001614920953453450247, 0.002422381430180175262, 0.003229841906906900494, 0.004037302383633626160, 0.004844762860360350525, 0.005652223337087076624, 0.006459683813813802723, 0.007267144290540529690, 0.008074604767267254055, 0.008882065243993981021, 0.009689525720720704519, 0.01049698619744742975, 0.01130444667417415498, 0.01211190715090088021, 0.01251563738926424196, 0.01291936762762760545 ),
 .UNSPECIFIED. ) ;
#1089=DIRECTION ( 'NONE',  ( 1.000000000000000000, -0.000000000000000000, -0.000000000000000000 ) ) ;
#1145=CARTESIAN_POINT ( 'NONE',  ( 0.000000000000000000, -100.0000000000000000, 0.000000000000000000 ) ) ;
#1146=CARTESIAN_POINT ( 'NONE',  ( 5.649205854336970312, -88.45354532811518311, -2.034449005107560549 ) ) ;
#1173=CARTESIAN_POINT ( 'NONE',  ( -4.472135954999578722, 249.9999999999999432, 4.000000000000002665 ) ) ;
#1221=CARTESIAN_POINT ( 'NONE',  ( -7.999912353029502654, -13.99982470603094065, -0.2691822806795001188 ) ) ;
#1321=CARTESIAN_POINT ( 'NONE',  ( 9.165151389911699198, 249.9999999999999432, -4.000000000000002665 ) ) ;
#1440=CARTESIAN_POINT ( 'NONE',  ( -5.999511540169428336, 246.0007326911455721, -0.2833228702578324265 ) ) ;
#1479=CARTESIAN_POINT ( 'NONE',  ( 5.855777637195783925, -81.21893503241551571, -1.331220292256681592 ) ) ;
#1616=CARTESIAN_POINT ( 'NONE',  ( -5.384233811324310892, -88.00217091344775611, 2.655407383564611923 ) ) ;
#1629=B_SPLINE_CURVE_WITH_KNOTS ( 'NONE', 3,
 ( #13810, #21418, #95819, #38652, #46205, #71519, #55328, #39707, #88255, #72582, #96871, #105485, #45676, #13277, #64511, #79091, #23538, #86682, #12753, #78556, #4686, #37619, #70482, #103377, #57443, #17558, #32692, #16477, #91444, #65559, #97919, #66619, #17021, #106000 ),
 .UNSPECIFIED., .F., .F.,
 ( 4, 2, 2, 2, 2, 2, 2, 2, 2, 2, 2, 2, 2, 2, 2, 2, 4 ),
 ( 1.734723475976807094E-18, 0.0007951492273476417835, 0.001590298454695281832, 0.002385447682042921881, 0.003180596909390559762, 0.003975746136738197642, 0.004770895364085835089, 0.005566044591433473403, 0.006361193818781110849, 0.007156343046128746561, 0.007951492273476384876, 0.008746641500824020588, 0.009541790728171659769, 0.01033693995551929548, 0.01113208918286693293, 0.01192723841021457037, 0.01272238763756220782 ),
 .UNSPECIFIED. ) ;
#1672=CARTESIAN_POINT ( 'NONE',  ( 6.943926999490791729, -84.46699007373852908, -3.973092371898547803 ) ) ;
#1690=ORIENTED_EDGE ( 'NONE', *, *, #35369, .F. ) ;
#1694=CYLINDRICAL_SURFACE ( 'NONE', #944, 4.000000000000002665 ) ;
#1751=EDGE_LOOP ( 'NONE', ( #16896, #102287, #65721, #16262 ) ) ;
#1967=CARTESIAN_POINT ( 'NONE',  ( 4.589925132946516939, -11.06526016292516523, 3.864926970398261830 ) ) ;
#2045=CARTESIAN_POINT ( 'NONE',  ( -7.414580834929597408, -7.353437197185189511, 3.010264818013838273 ) ) ;
#2058=CARTESIAN_POINT ( 'NONE',  ( 6.944031699373467426, -65.53460654556130294, 3.972913591453824278 ) ) ;
#2070=CARTESIAN_POINT ( 'NONE',  ( 5.092539576892236575, 247.5567653279156843, 3.177249149099067083 ) ) ;
#2178=CARTESIAN_POINT ( 'NONE',  ( -7.414580834929595632, -62.35343719718518685, 3.010264818013839161 ) ) ;
#2221=DIRECTION ( 'NONE',  ( 0.000000000000000000, 0.000000000000000000, -1.000000000000000000 ) ) ;
#2406=CARTESIAN_POINT ( 'NONE',  ( 9.482993638194562536, 247.5565127974631423, -3.177441187500463116 ) ) ;
#2453=CARTESIAN_POINT ( 'NONE',  ( 5.650483388624512493, 253.4556659685037801, 2.031129859422152073 ) ) ;
#2482=CARTESIAN_POINT ( 'NONE',  ( 7.151217271224854954, -63.21250599554285543, -3.587901469523285591 ) ) ;
#2490=CARTESIAN_POINT ( 'NONE',  ( -4.904566723942682671, -82.97757297529254572, 3.460360782932704549 ) ) ;
#2514=CARTESIAN_POINT ( 'NONE',  ( -4.905194654929163178, 247.9760560498015423, 3.459476078998869220 ) ) ;
#2564=EDGE_CURVE ( 'NONE', #4789, #50935, #13795, .T. ) ;
#2575=VERTEX_POINT ( 'NONE', #46676 ) ;
#2578=CARTESIAN_POINT ( 'NONE',  ( -6.928203230275510549, -9.731166754910027805, -4.000000000000000888 ) ) ;
#2601=STYLED_ITEM ( 'NONE', ( #56556 ), #88119 ) ;
#2608=CARTESIAN_POINT ( 'NONE',  ( 5.725989721596479676, 246.4232288874353287, 1.809923354557179564 ) ) ;
#2656=DIRECTION ( 'NONE',  ( 1.000000000000000000, -0.000000000000000000, -0.000000000000000000 ) ) ;
#2689=CARTESIAN_POINT ( 'NONE',  ( 9.483056940782045530, 252.4438779010656617, -3.177305548492613596 ) ) ;
#2697=PLANE ( 'NONE',  #4168 ) ;
#2721=CARTESIAN_POINT ( 'NONE',  ( 7.344361273354515163, -12.44560530588525538, -3.175733139645583236 ) ) ;
#2800=CARTESIAN_POINT ( 'NONE',  ( -5.856955515201470064, 253.7828905888086410, 1.326217528971443294 ) ) ;
#2913=CIRCLE ( 'NONE', #99363, 12.00000000000003908 ) ;
#2920=AXIS2_PLACEMENT_3D ( 'NONE', #53793, #102886, #79128 ) ;
#2936=CARTESIAN_POINT ( 'NONE',  ( 9.253800200985700997, 248.6998966891182192, -3.791983798715486742 ) ) ;
#3021=CARTESIAN_POINT ( 'NONE',  ( -4.472135954999578722, 249.9999999999999432, 4.000000000000002665 ) ) ;
#3024=CARTESIAN_POINT ( 'NONE',  ( 7.211357414135266986, -62.98853460065557641, 3.467230644691331687 ) ) ;
#3033=CARTESIAN_POINT ( 'NONE',  ( -5.856955515201466511, -81.21710941119138738, 1.326217528971465942 ) ) ;
#3091=CARTESIAN_POINT ( 'NONE',  ( -9.797537890442951536, 246.5344220233380099, 2.014215961808872635 ) ) ;
#3234=CARTESIAN_POINT ( 'NONE',  ( 9.380871178326138704, 252.0111637979832153, 3.467392232194206780 ) ) ;
#3268=CARTESIAN_POINT ( 'NONE',  ( -5.647817967127097383, -68.45126406528792984, -2.038183545141174058 ) ) ;
#3289=CARTESIAN_POINT ( 'NONE',  ( 7.002641335706725201, -83.94912737319167206, 3.868676264653294172 ) ) ;
#3313=CARTESIAN_POINT ( 'NONE',  ( -7.212408192734265810, -67.01517089320368825, -3.465038817813883121 ) ) ;
#3345=CARTESIAN_POINT ( 'NONE',  ( -4.496882872040836254, 250.5378866548961696, 3.972797206970395845 ) ) ;
#3364=EDGE_LOOP ( 'NONE', ( #96309, #65907 ) ) ;
#3481=CARTESIAN_POINT ( 'NONE',  ( -5.855777637195783925, -13.78106496758447719, -1.331220292256675597 ) ) ;
#3577=CARTESIAN_POINT ( 'NONE',  ( -5.981691436642414317, -81.02730900805887870, -0.5384679144502629855 ) ) ;
#3589=CARTESIAN_POINT ( 'NONE',  ( -7.046289519167717508, -86.30591819944376653, -3.789821819998814512 ) ) ;
#3595=CARTESIAN_POINT ( 'NONE',  ( -5.999787407977320797, -61.00031888815551895, 0.2740427891042978015 ) ) ;
#3613=SURFACE_STYLE_USAGE ( .BOTH. , #20380 ) ;
#3665=CARTESIAN_POINT ( 'NONE',  ( -7.934996450857311423, -6.131375435274703634, -1.050865690281775899 ) ) ;
#3697=CARTESIAN_POINT ( 'NONE',  ( 4.497431761510337189, -9.459018757489689122, -3.972160586670082871 ) ) ;
#3774=CARTESIAN_POINT ( 'NONE',  ( 9.645512969475877441, 253.0110315067572913, -2.645801731561389314 ) ) ;
#3794=AXIS2_PLACEMENT_3D ( 'NONE', #9552, #27400, #67812 ) ;
#3801=CARTESIAN_POINT ( 'NONE',  ( 7.212994264445062420, -12.01711344340039567, 3.463766307298584923 ) ) ;
#3853=CARTESIAN_POINT ( 'NONE',  ( -6.928203230275508773, -65.00000000000000000, 4.000000000000002665 ) ) ;
#4007=CARTESIAN_POINT ( 'NONE',  ( -5.093082057083965886, -12.44446206421571866, -3.176439207277719223 ) ) ;
#4080=LINE ( 'NONE', #39113, #39339 ) ;
#4099=CARTESIAN_POINT ( 'NONE',  ( 6.943926999490791729, -64.46699007373854329, -3.973092371898547803 ) ) ;
#4107=CARTESIAN_POINT ( 'NONE',  ( -4.813668318631095566, -83.20486770173317836, 3.583991016754781711 ) ) ;
#4111=VERTEX_POINT ( 'NONE', #104586 ) ;
#4118=CARTESIAN_POINT ( 'NONE',  ( -7.800703710507056243, -88.58595692657942777, 1.791736796405269061 ) ) ;
#4124=CARTESIAN_POINT ( 'NONE',  ( -5.477578620271507326, -61.83498560983895231, -2.459398706554657199 ) ) ;
#4142=( LENGTH_UNIT ( ) NAMED_UNIT ( * ) SI_UNIT ( .MILLI., .METRE. ) );
#4168=AXIS2_PLACEMENT_3D ( 'NONE', #93317, #18935, #84691 ) ;
#4177=EDGE_LOOP ( 'NONE', ( #61258, #17732 ) ) ;
#4217=CARTESIAN_POINT ( 'NONE',  ( 5.858881034796412202, -6.214136759970199542, 1.317748741875969243 ) ) ;
#4284=EDGE_CURVE ( 'NONE', #41649, #68317, #63775, .T. ) ;
#4295=CARTESIAN_POINT ( 'NONE',  ( 5.476751506168961114, -61.83642877133009108, -2.461144630687909451 ) ) ;
#4296=CARTESIAN_POINT ( 'NONE',  ( 9.918579450955592236, 253.7930391296868606, 1.297207292923829636 ) ) ;
#4326=CARTESIAN_POINT ( 'NONE',  ( 7.002990960197235104, -11.05266818383458016, 3.868040364119523566 ) ) ;
#4349=CARTESIAN_POINT ( 'NONE',  ( 7.934883677559678716, -81.13160822062448574, 1.051380792122687202 ) ) ;
#4371=CARTESIAN_POINT ( 'NONE',  ( -7.618844049274131613, -68.17235898929459381, 2.450177051822849172 ) ) ;
#4401=CARTESIAN_POINT ( 'NONE',  ( -4.595881407952570719, 251.0662543320131874, -3.857520671226069897 ) ) ;
#4465=ADVANCED_FACE ( 'NONE', ( #45708 ), #47284, .F. ) ;
#4601=UNCERTAINTY_MEASURE_WITH_UNIT (LENGTH_MEASURE( 1.000000000000000082E-05 ), #46399, 'distance_accuracy_value', 'NONE');
#4612=CARTESIAN_POINT ( 'NONE',  ( 6.928203230275509661, -65.00000000000000000, -4.000000000000002665 ) ) ;
#4642=CARTESIAN_POINT ( 'NONE',  ( -5.191144708981714651, -82.35969914478735632, 3.015512395308853844 ) ) ;
#4658=CARTESIAN_POINT ( 'NONE',  ( -5.475947152006324536, -61.83782269890877359, 2.462898245435129585 ) ) ;
#4686=CARTESIAN_POINT ( 'NONE',  ( 7.896571385775229324, -6.210020006542475990, 1.305932416347438618 ) ) ;
#4728=( LENGTH_UNIT ( ) NAMED_UNIT ( * ) SI_UNIT ( .MILLI., .METRE. ) );
#4749=CARTESIAN_POINT ( 'NONE',  ( 4.472135954999581386, -10.00000000000000888, -4.000000000000000000 ) ) ;
#4789=VERTEX_POINT ( 'NONE', #19240 ) ;
#4984=CARTESIAN_POINT ( 'NONE',  ( 5.475947152006326313, -68.16217730109124773, 2.462898245435125588 ) ) ;
#5069=CARTESIAN_POINT ( 'NONE',  ( -4.589357672516648279, -11.06206030977222809, -3.865585121226768894 ) ) ;
#5181=CARTESIAN_POINT ( 'NONE',  ( -6.928203230275508773, -85.00000000000000000, 4.000000000000001776 ) ) ;
#5286=TOROIDAL_SURFACE ( 'NONE', #82726, 12.00000000000003908, 1.000000000000000000 ) ;
#5342=CARTESIAN_POINT ( 'NONE',  ( 9.165151389911697422, 249.7370448908366143, 4.000000000000004441 ) ) ;
#5365=CARTESIAN_POINT ( 'NONE',  ( 5.909259836070534178, -61.13722795757932715, -1.072443315311459200 ) ) ;
#5393=CARTESIAN_POINT ( 'NONE',  ( -4.815811321232738251, -66.80076707697375582, 3.581116321197038932 ) ) ;
#5507=CARTESIAN_POINT ( 'NONE',  ( 5.727189096784631062, -68.57869875248739788, -1.806430436190349376 ) ) ;
#5539=VERTEX_POINT ( 'NONE', #5982 ) ;
#5563=ORIENTED_EDGE ( 'NONE', *, *, #24288, .F. ) ;
#5578=B_SPLINE_CURVE_WITH_KNOTS ( 'NONE', 3,
 ( #67265, #93662, #85580, #1967, #60254, #68323, #67784, #100144, #25780, #27374, #50514, #59706, #43512, #100672, #76391, #26835, #26309, #19812, #92583, #11655, #36525, #18738, #19294, #42437, #93121, #52118, #35994, #10595, #68866, #58638, #52649, #77475, #91538, #17651, #78000, #88223 ),
 .UNSPECIFIED., .F., .F.,
 ( 4, 2, 2, 2, 2, 2, 2, 2, 2, 2, 2, 2, 2, 2, 2, 2, 2, 4 ),
 ( 0.01291936762762759330, 0.01372441420841340187, 0.01452946078919920871, 0.01533450736998501727, 0.01613955395077082411, 0.01694460053155663268, 0.01774964711234244125, 0.01855469369312824982, 0.01935974027391405838, 0.02016478685469986348, 0.02096983343548567205, 0.02177488001627148062, 0.02257992659705728572, 0.02338497317784309429, 0.02419001975862890286, 0.02459254304902180888, 0.02499506633941471143, 0.02580011292020051999 ),
 .UNSPECIFIED. ) ;
#5593=CARTESIAN_POINT ( 'NONE',  ( -5.190609988845228173, -12.63922286743592593, -3.016375611400007539 ) ) ;
#5636=CARTESIAN_POINT ( 'NONE',  ( 0.000000000000000000, 4.000000000000003553, 0.000000000000000000 ) ) ;
#5664=CARTESIAN_POINT ( 'NONE',  ( 0.000000000000000000, 299.9999999999999432, 6.000000000000000888 ) ) ;
#5741=CARTESIAN_POINT ( 'NONE',  ( -9.165151389911699198, 249.9999999999999432, 4.000000000000002665 ) ) ;
#5798=FACE_BOUND ( 'NONE', #4177, .T. ) ;
#5870=CARTESIAN_POINT ( 'NONE',  ( 5.384233811324311780, -61.99782908655225810, 2.655407383564610146 ) ) ;
#5982=CARTESIAN_POINT ( 'NONE',  ( 0.000000000000000000, 3.999999999999996447, 12.00000000000003908 ) ) ;
#6021=CARTESIAN_POINT ( 'NONE',  ( 4.472135954999578722, -65.27077220067361907, 4.000000000000002665 ) ) ;
#6151=CARTESIAN_POINT ( 'NONE',  ( -7.896165657598944065, -13.78911131371973653, -1.307894402814546719 ) ) ;
#6245=ORIENTED_EDGE ( 'NONE', *, *, #69895, .F. ) ;
#6255=CARTESIAN_POINT ( 'NONE',  ( -9.165151389911699198, 249.7368049370512324, 4.000000000000006217 ) ) ;
#6394=EDGE_LOOP ( 'NONE', ( #5563, #15262, #68158, #89923 ) ) ;
#6401=EDGE_CURVE ( 'NONE', #38536, #25105, #1629, .T. ) ;
#6510=CARTESIAN_POINT ( 'NONE',  ( -13.00000000000003730, -65.00000000000000000, 4.000000000000002665 ) ) ;
#6521=CARTESIAN_POINT ( 'NONE',  ( 0.000000000000000000, 3.999999999999996447, -10.00000000000003730 ) ) ;
#6532=LINE ( 'NONE', #31395, #12767 ) ;
#6771=EDGE_LOOP ( 'NONE', ( #10359, #69863 ) ) ;
#6786=UNCERTAINTY_MEASURE_WITH_UNIT (LENGTH_MEASURE( 1.000000000000000082E-05 ), #63979, 'distance_accuracy_value', 'NONE');
#6803=DIRECTION ( 'NONE',  ( 1.000000000000000000, -0.000000000000000000, -0.000000000000000000 ) ) ;
#7193=EDGE_CURVE ( 'NONE', #84992, #101817, #102152, .T. ) ;
#7198=VECTOR ( 'NONE', #74642, 1000.000000000000000 ) ;
#7211=ORIENTED_EDGE ( 'NONE', *, *, #13896, .T. ) ;
#7215=CARTESIAN_POINT ( 'NONE',  ( -6.943926999490789065, -10.53300992626148869, -3.973092371898544251 ) ) ;
#7381=CARTESIAN_POINT ( 'NONE',  ( 4.905194654929169396, -7.976056049801584891, 3.459476078998858117 ) ) ;
#7382=FACE_BOUND ( 'NONE', #58866, .T. ) ;
#7460=EDGE_LOOP ( 'NONE', ( #94887, #63977 ) ) ;
#7583=CARTESIAN_POINT ( 'NONE',  ( -4.497431761510337189, -85.54098124251034108, -3.972160586670088200 ) ) ;
#7658=CARTESIAN_POINT ( 'NONE',  ( 5.382954851612917757, -87.99987491489449098, -2.657971597726724866 ) ) ;
#7860=ORIENTED_EDGE ( 'NONE', *, *, #69895, .T. ) ;
#8025=CARTESIAN_POINT ( 'NONE',  ( 7.414580834929597408, -67.64656280281481315, 3.010264818013837385 ) ) ;
#8027=CYLINDRICAL_SURFACE ( 'NONE', #53713, 6.000000000000000888 ) ;
#8125=CARTESIAN_POINT ( 'NONE',  ( -5.999511540169428336, -88.99926730885431425, -0.2833228702578375335 ) ) ;
#8172=EDGE_LOOP ( 'NONE', ( #12389, #50517, #66629, #30330 ) ) ;
#8203=CARTESIAN_POINT ( 'NONE',  ( 4.472135954999579610, -85.00000000000000000, -4.000000000000001776 ) ) ;
#8276=CARTESIAN_POINT ( 'NONE',  ( -8.000086790516059310, -14.00017358106007137, 0.2639471549312823462 ) ) ;
#8421=CARTESIAN_POINT ( 'NONE',  ( -9.177080501238330967, 250.5334694285427020, -3.972956046786637607 ) ) ;
#8434=EDGE_LOOP ( 'NONE', ( #19804, #40270 ) ) ;
#8450=AXIS2_PLACEMENT_3D ( 'NONE', #94386, #11305, #45303 ) ;
#8519=CARTESIAN_POINT ( 'NONE',  ( 5.192560085536412906, -82.35694557368756819, 3.013051918867554413 ) ) ;
#8731=FACE_OUTER_BOUND ( 'NONE', #32713, .T. ) ;
#8739=CARTESIAN_POINT ( 'NONE',  ( -7.046289519167719284, -66.30591819944378074, -3.789821819998816288 ) ) ;
#8809=CARTESIAN_POINT ( 'NONE',  ( -7.743982712349853692, -13.46213014760737181, 2.020119794285908377 ) ) ;
#8840=VECTOR ( 'NONE', #106493, 1000.000000000000000 ) ;
#8902=CARTESIAN_POINT ( 'NONE',  ( 9.176803346051531918, 249.4705284420255680, 3.973598758023531019 ) ) ;
#8949=CARTESIAN_POINT ( 'NONE',  ( 4.472135954999581386, -10.00000000000000888, -4.000000000000000000 ) ) ;
#9178=CARTESIAN_POINT ( 'NONE',  ( -5.855777637195783925, -88.78106496758448429, -1.331220292256681592 ) ) ;
#9208=CARTESIAN_POINT ( 'NONE',  ( -7.213352437320215138, -62.98163526992318850, -3.463014597543483841 ) ) ;
#9227=ORIENTED_EDGE ( 'NONE', *, *, #22034, .T. ) ;
#9257=CARTESIAN_POINT ( 'NONE',  ( 5.981691436642414317, -88.97269099194117814, -0.5384679144502629855 ) ) ;
#9471=CARTESIAN_POINT ( 'NONE',  ( -9.165151389911699198, 249.9999999999999716, -4.000000000000002665 ) ) ;
#9537=CARTESIAN_POINT ( 'NONE',  ( -4.903871675326607615, 247.9791419269849087, -3.461400506969853019 ) ) ;
#9552=CARTESIAN_POINT ( 'NONE',  ( 0.000000000000000000, 299.9999999999999432, 0.000000000000000000 ) ) ;
#9568=FACE_OUTER_BOUND ( 'NONE', #74486, .T. ) ;
#9574=CARTESIAN_POINT ( 'NONE',  ( 4.590682673078522846, -83.93208242687842358, 3.864023243754608483 ) ) ;
#9593=ORIENTED_EDGE ( 'NONE', *, *, #33326, .T. ) ;
#9629=CARTESIAN_POINT ( 'NONE',  ( 5.727189096784626621, 246.4213012475125311, -1.806430436190365585 ) ) ;
#9736=CARTESIAN_POINT ( 'NONE',  ( -7.744168461338430731, -61.53745938284842509, 2.019395720771554270 ) ) ;
#9895=ADVANCED_FACE ( 'NONE', ( #83425 ), #76930, .F. ) ;
#9914=STYLED_ITEM ( 'NONE', ( #81206 ), #58495 ) ;
#9960=( NAMED_UNIT ( * ) SI_UNIT ( $, .STERADIAN. ) SOLID_ANGLE_UNIT ( ) );
#9978=DIRECTION ( 'NONE',  ( 1.000000000000000000, -0.000000000000000000, -0.000000000000000000 ) ) ;
#9985=AXIS2_PLACEMENT_3D ( 'NONE', #60606, #43863, #84330 ) ;
#10020=CARTESIAN_POINT ( 'NONE',  ( 4.656749229489900443, 251.3176040812644203, -3.785628640239131038 ) ) ;
#10115=CARTESIAN_POINT ( 'NONE',  ( -10.00005432054558341, 245.9998641986207701, 0.2621623937322782871 ) ) ;
#10120=CARTESIAN_POINT ( 'NONE',  ( 4.905194654929173836, -82.97605604980155647, 3.459476078998853676 ) ) ;
#10144=CARTESIAN_POINT ( 'NONE',  ( -6.928203230275509661, -9.735207327464285854, 3.999999999999999112 ) ) ;
#10158=CARTESIAN_POINT ( 'NONE',  ( 6.928203230275509661, -65.26479267253573369, 4.000000000000002665 ) ) ;
#10205=CARTESIAN_POINT ( 'NONE',  ( -13.00000000000003730, -85.00000000000000000, 4.000000000000001776 ) ) ;
#10359=ORIENTED_EDGE ( 'NONE', *, *, #36291, .F. ) ;
#10422=CARTESIAN_POINT ( 'NONE',  ( -5.858824175751780494, -6.214209391276424022, -1.318356988357135107 ) ) ;
#10585=CARTESIAN_POINT ( 'NONE',  ( -4.660674839411966808, -83.68217514695594161, -3.778981567323765223 ) ) ;
#10591=CARTESIAN_POINT ( 'NONE',  ( -13.00000000000003730, -65.00000000000000000, 0.000000000000000000 ) ) ;
#10595=CARTESIAN_POINT ( 'NONE',  ( 4.905018583967753365, -12.02359985679681742, -3.459768807258289502 ) ) ;
#10665=CARTESIAN_POINT ( 'NONE',  ( -7.002990960197235104, -8.947331816165435825, 3.868040364119522234 ) ) ;
#10679=CARTESIAN_POINT ( 'NONE',  ( 7.344361273354517827, -67.44560530588525182, -3.175733139645580128 ) ) ;
#10694=CARTESIAN_POINT ( 'NONE',  ( 4.814352310392297163, 248.2032140589641642, -3.583053941560760958 ) ) ;
#10728=AXIS2_PLACEMENT_3D ( 'NONE', #14983, #57033, #47878 ) ;
#10768=CARTESIAN_POINT ( 'NONE',  ( 9.176855344543007220, 250.5296042697742109, -3.973472207155925862 ) ) ;
#10799=CARTESIAN_POINT ( 'NONE',  ( 7.619135598915497631, -13.17305367784679859, 2.449260492474792272 ) ) ;
#11096=CARTESIAN_POINT ( 'NONE',  ( 7.896571385775229324, -61.21002000654245734, 1.305932416347441505 ) ) ;
#11104=CARTESIAN_POINT ( 'NONE',  ( -4.472135954999579610, -85.00000000000000000, -4.000000000000001776 ) ) ;
#11123=CARTESIAN_POINT ( 'NONE',  ( -5.727189096784631062, -61.42130124751258791, -1.806430436190351374 ) ) ;
#11127=CARTESIAN_POINT ( 'NONE',  ( -5.909259836070535066, 246.1372279575791993, -1.072443315311452539 ) ) ;
#11135=CARTESIAN_POINT ( 'NONE',  ( 7.986468734911285949, -88.97313679723080782, 0.5341897780976099241 ) ) ;
#11161=CARTESIAN_POINT ( 'NONE',  ( -9.918579450955581578, 246.2069608703131109, 1.297207292923867827 ) ) ;
#11205=CARTESIAN_POINT ( 'NONE',  ( 7.801777176595948937, -68.58827985812635575, -1.786991866639918936 ) ) ;
#11224=CARTESIAN_POINT ( 'NONE',  ( 4.595881407952560060, 248.9337456679867842, -3.857520671226082776 ) ) ;
#11301=CARTESIAN_POINT ( 'NONE',  ( 5.382057749264594904, -62.00173201596057027, -2.659775980967110431 ) ) ;
#11305=DIRECTION ( 'NONE',  ( 1.000000000000000000, 0.000000000000000000, -1.224646799147353207E-16 ) ) ;
#11317=B_SPLINE_CURVE_WITH_KNOTS ( 'NONE', 3,
 ( #96908, #74733, #74205, #73130, #24110, #99002, #106034, #283, #33251, #66123, #73674, #15443, #55876, #80702, #58022, #97412, #57482, #88811, #24635, #106577, #81752, #98482, #32181, #32729, #90949, #23572, #17057, #40781, #82304, #65596, #49936, #90407, #82841, #16510 ),
 .UNSPECIFIED., .F., .F.,
 ( 4, 2, 2, 2, 2, 2, 2, 2, 2, 2, 2, 2, 2, 2, 2, 2, 4 ),
 ( 0.01272238763756221476, 0.01351613129786393384, 0.01430987495816565119, 0.01510361861846737028, 0.01589736227876908936, 0.01669110593907080844, 0.01748484959937252753, 0.01827859325967424314, 0.01907233691997596223, 0.01986608058027768131, 0.02065982424057940040, 0.02145356790088111948, 0.02224731156118283509, 0.02304105522148455765, 0.02383479888178627326, 0.02462854254208799235, 0.02542228620238971143 ),
 .UNSPECIFIED. ) ;
#11346=AXIS2_PLACEMENT_3D ( 'NONE', #6521, #47516, #38402 ) ;
#11347=CARTESIAN_POINT ( 'NONE',  ( 0.000000000000000000, 1.000000000000000888, 0.000000000000000000 ) ) ;
#11353=CARTESIAN_POINT ( 'NONE',  ( 7.986539162393897939, -81.02672828942547767, -0.5321833565149911571 ) ) ;
#11390=DIRECTION ( 'NONE',  ( -0.000000000000000000, -1.000000000000000000, -0.000000000000000000 ) ) ;
#11411=CARTESIAN_POINT ( 'NONE',  ( -5.477578620271503773, 253.1650143901609908, -2.459398706554668745 ) ) ;
#11440=UNCERTAINTY_MEASURE_WITH_UNIT (LENGTH_MEASURE( 1.000000000000000082E-05 ), #73649, 'distance_accuracy_value', 'NONE');
#11512=CARTESIAN_POINT ( 'NONE',  ( 0.000000000000000000, -100.0000000000000000, 0.000000000000000000 ) ) ;
#11552=CARTESIAN_POINT ( 'NONE',  ( 9.843481099141470736, 246.4079544384660494, -1.779148000612204017 ) ) ;
#11602=CARTESIAN_POINT ( 'NONE',  ( 4.658465013329196047, 251.3236387967309327, 3.783534922165387115 ) ) ;
#11635=CARTESIAN_POINT ( 'NONE',  ( 6.928203230275507885, -64.73473843067414180, 4.000000000000002665 ) ) ;
#11655=CARTESIAN_POINT ( 'NONE',  ( 5.910690929868577470, -13.86495906093194463, -1.065041252563911467 ) ) ;
#11657=CARTESIAN_POINT ( 'NONE',  ( -6.928203230275507885, -85.00000000000000000, -4.000000000000001776 ) ) ;
#11724=CARTESIAN_POINT ( 'NONE',  ( -6.944371705245973025, -9.461003085754503772, -3.972324460300561633 ) ) ;
#11841=CARTESIAN_POINT ( 'NONE',  ( 9.989285784994834216, 253.9734242744569030, 0.5301777604595797611 ) ) ;
#11949=CARTESIAN_POINT ( 'NONE',  ( -4.660674839411965031, 251.3178248530441010, -3.778981567323766555 ) ) ;
#12014=CARTESIAN_POINT ( 'NONE',  ( -5.910690929868578358, -6.135040939068072241, -1.065041252563909913 ) ) ;
#12025=AXIS2_PLACEMENT_3D ( 'NONE', #81269, #47315, #71069 ) ;
#12081=ORIENTED_EDGE ( 'NONE', *, *, #49730, .T. ) ;
#12084=CARTESIAN_POINT ( 'NONE',  ( -4.813555570991615795, -11.79473796517323159, -3.584128953194782419 ) ) ;
#12111=AXIS2_PLACEMENT_3D ( 'NONE', #64850, #83158, #24435 ) ;
#12120=ORIENTED_EDGE ( 'NONE', *, *, #4284, .T. ) ;
#12171=CARTESIAN_POINT ( 'NONE',  ( 6.928203230275506108, -64.73069070304460126, -4.000000000000002665 ) ) ;
#12179=CARTESIAN_POINT ( 'NONE',  ( -4.589925132946516939, -83.93473983707484365, 3.864926970398267603 ) ) ;
#12193=CARTESIAN_POINT ( 'NONE',  ( -7.551437640244095917, -88.00872462522907824, -2.648272645923386737 ) ) ;
#12199=CARTESIAN_POINT ( 'NONE',  ( -5.858824175751781382, -61.21420939127642669, -1.318356988357135773 ) ) ;
#12245=AXIS2_PLACEMENT_3D ( 'NONE', #96058, #71234, #104130 ) ;
#12281=CARTESIAN_POINT ( 'NONE',  ( 7.986711519608433285, -68.97361903623433932, -0.5300249774147592907 ) ) ;
#12373=CARTESIAN_POINT ( 'NONE',  ( 9.797537890442953312, 253.4655779766619048, 2.014215961808876632 ) ) ;
#12389=ORIENTED_EDGE ( 'NONE', *, *, #14871, .F. ) ;
#12400=CARTESIAN_POINT ( 'NONE',  ( 7.744168461338432508, -13.46254061715158379, 2.019395720771548053 ) ) ;
#12418=DIRECTION ( 'NONE',  ( -0.000000000000000000, -1.000000000000000000, -0.000000000000000000 ) ) ;
#12423=CARTESIAN_POINT ( 'NONE',  ( 8.000086790516061086, -80.99982641893991797, 0.2639471549312816800 ) ) ;
#12493=CYLINDRICAL_SURFACE ( 'NONE', #89172, 13.00000000000003730 ) ;
#12506=CARTESIAN_POINT ( 'NONE',  ( -9.165151389911699198, 249.9999999999999716, -4.000000000000002665 ) ) ;
#12537=CARTESIAN_POINT ( 'NONE',  ( -5.477578620271509102, -6.834985609838969189, -2.459398706554655423 ) ) ;
#12607=EDGE_CURVE ( 'NONE', #104803, #78936, #40722, .T. ) ;
#12686=LINE ( 'NONE', #76356, #64469 ) ;
#12726=VERTEX_POINT ( 'NONE', #72921 ) ;
#12727=CARTESIAN_POINT ( 'NONE',  ( -5.856955515201466511, -61.21710941119133764, 1.326217528971461279 ) ) ;
#12746=PLANE ( 'NONE',  #42707 ) ;
#12753=CARTESIAN_POINT ( 'NONE',  ( 7.986452802927059835, -6.026902423081146765, 0.5332468218996346820 ) ) ;
#12767=VECTOR ( 'NONE', #82008, 1000.000000000000000 ) ;
#12808=CARTESIAN_POINT ( 'NONE',  ( 7.744329845603314944, -68.46288230153457732, -2.018701143083234228 ) ) ;
#12931=CARTESIAN_POINT ( 'NONE',  ( -5.382057749264594904, -67.99826798403944395, -2.659775980967107767 ) ) ;
#12951=CARTESIAN_POINT ( 'NONE',  ( 7.412906595240168706, -82.35811727147745387, 3.014362223629233561 ) ) ;
#12979=CYLINDRICAL_SURFACE ( 'NONE', #97911, 4.000000000000001776 ) ;
#13046=CARTESIAN_POINT ( 'NONE',  ( 4.905018583967751589, -67.02359985679677834, -3.459768807258292167 ) ) ;
#13065=AXIS2_PLACEMENT_3D ( 'NONE', #27579, #91742, #93337 ) ;
#13180=CARTESIAN_POINT ( 'NONE',  ( -6.928203230275509661, -10.26930929695540229, -4.000000000000000000 ) ) ;
#13183=DIRECTION ( 'NONE',  ( 0.000000000000000000, 0.000000000000000000, -1.000000000000000000 ) ) ;
#13193=CARTESIAN_POINT ( 'NONE',  ( 4.472135954999580498, 250.1357920494656355, 4.000000000000003553 ) ) ;
#13248=CARTESIAN_POINT ( 'NONE',  ( -8.000086790516061086, -89.00017358106008203, 0.2639471549312816800 ) ) ;
#13267=ORIENTED_EDGE ( 'NONE', *, *, #78931, .F. ) ;
#13277=CARTESIAN_POINT ( 'NONE',  ( 7.896165657598944065, -6.210888686280283011, -1.307894402814547163 ) ) ;
#13426=CARTESIAN_POINT ( 'NONE',  ( 4.589357672516644726, -63.93793969022779322, -3.865585121226772447 ) ) ;
#13459=CARTESIAN_POINT ( 'NONE',  ( -5.093234209761996034, -67.44467773464910465, 3.176141468578046467 ) ) ;
#13481=CARTESIAN_POINT ( 'NONE',  ( 7.344505440741524893, -82.55381072701295864, -3.175463080953003558 ) ) ;
#13484=ADVANCED_FACE ( 'NONE', ( #106386 ), #65946, .F. ) ;
#13565=ORIENTED_EDGE ( 'NONE', *, *, #61572, .T. ) ;
#13566=EDGE_CURVE ( 'NONE', #22177, #53932, #28357, .T. ) ;
#13581=CARTESIAN_POINT ( 'NONE',  ( 5.383284837158154090, -68.00049343515777878, 2.657356347551696363 ) ) ;
#13632=CARTESIAN_POINT ( 'NONE',  ( 4.472135954999579610, -85.27077220067363328, 4.000000000000002665 ) ) ;
#13794=CYLINDRICAL_SURFACE ( 'NONE', #48909, 13.00000000000003730 ) ;
#13795=B_SPLINE_CURVE_WITH_KNOTS ( 'NONE', 3,
 ( #45633, #27363, #78508, #12179, #44574, #4107, #2490, #76922, #4642, #77464, #35439, #18723, #68310, #3033, #60241, #37034, #94180, #70437, #3577, #69902, #102801, #69380, #61832, #51577, #29479, #92573, #36512, #35982, #93110, #84493, #10585, #102262, #19283, #52109, #85021, #11104 ),
 .UNSPECIFIED., .F., .F.,
 ( 4, 2, 2, 2, 2, 2, 2, 2, 2, 2, 2, 2, 2, 2, 2, 2, 2, 4 ),
 ( 0.01291936762762758983, 0.01372441420841339667, 0.01452946078919920350, 0.01533450736998501034, 0.01613955395077081717, 0.01694460053155662227, 0.01774964711234243084, 0.01855469369312823594, 0.01935974027391404451, 0.02016478685469984961, 0.02096983343548565470, 0.02177488001627146327, 0.02257992659705727184, 0.02338497317784307694, 0.02419001975862888204, 0.02459254304902178806, 0.02499506633941468714, 0.02580011292020053387 ),
 .UNSPECIFIED. ) ;
#13803=DIRECTION ( 'NONE',  ( 0.000000000000000000, 0.000000000000000000, -1.000000000000000000 ) ) ;
#13810=CARTESIAN_POINT ( 'NONE',  ( 6.928203230275508773, -10.00000000000001066, -4.000000000000000000 ) ) ;
#13862=ORIENTED_EDGE ( 'NONE', *, *, #49055, .T. ) ;
#13875=FACE_OUTER_BOUND ( 'NONE', #98099, .T. ) ;
#13896=EDGE_CURVE ( 'NONE', #36313, #65228, #104352, .T. ) ;
#13914=ORIENTED_EDGE ( 'NONE', *, *, #66865, .F. ) ;
#14066=CARTESIAN_POINT ( 'NONE',  ( -4.472135954999577834, 250.2732990351264561, -4.000000000000002665 ) ) ;
#14107=CARTESIAN_POINT ( 'NONE',  ( 5.910690929868579246, -68.86495906093195174, -1.065041252563907248 ) ) ;
#14255=CARTESIAN_POINT ( 'NONE',  ( 4.590682673078532616, 251.0679175731215764, 3.864023243754595605 ) ) ;
#14494=SURFACE_STYLE_FILL_AREA ( #23703 ) ;
#14633=CARTESIAN_POINT ( 'NONE',  ( 5.477578620271509990, -68.16501439016104769, -2.459398706554655867 ) ) ;
#14699=ORIENTED_EDGE ( 'NONE', *, *, #94152, .F. ) ;
#14844=B_SPLINE_CURVE_WITH_KNOTS ( 'NONE', 3,
 ( #18235, #52165, #34961, #50553, #68910, #36568, #100188, #67828, #59215, #75374, #19859, #76975, #26355, #76434, #85077, #35492, #51089, #10115, #100715, #59751, #11161, #84550, #3091, #27416, #93169, #36038, #72068, #69958, #37628, #86166, #104429, #29533, #6255, #5741 ),
 .UNSPECIFIED., .F., .F.,
 ( 4, 2, 2, 2, 2, 2, 2, 2, 2, 2, 2, 2, 2, 2, 2, 2, 4 ),
 ( 2.814585498623475875E-17, 0.0007899309203816313628, 0.001579861840763234536, 0.002369792761144837601, 0.003159723681526440883, 0.003949654601908043731, 0.004739585522289646580, 0.005529516442671250295, 0.006319447363052853144, 0.007109378283434455992, 0.007899309203816059707, 0.008689240124197663423, 0.009479171044579265404, 0.01026910196496086912, 0.01105903288534247284, 0.01184896380572407482, 0.01263889472610567853 ),
 .UNSPECIFIED. ) ;
#14860=EDGE_CURVE ( 'NONE', #19102, #94625, #32154, .T. ) ;
#14871=EDGE_CURVE ( 'NONE', #76918, #33707, #78538, .T. ) ;
#14873=EDGE_LOOP ( 'NONE', ( #70025, #97365 ) ) ;
#14885=CYLINDRICAL_SURFACE ( 'NONE', #97755, 4.000000000000000000 ) ;
#14983=CARTESIAN_POINT ( 'NONE',  ( 0.000000000000000000, 0.000000000000000000, 0.000000000000000000 ) ) ;
#15024=CARTESIAN_POINT ( 'NONE',  ( 5.858881034796412202, -61.21413675997018800, 1.317748741875967022 ) ) ;
#15052=ADVANCED_FACE ( 'NONE', ( #62815 ), #103786, .F. ) ;
#15246=ORIENTED_EDGE ( 'NONE', *, *, #78931, .T. ) ;
#15262=ORIENTED_EDGE ( 'NONE', *, *, #57076, .T. ) ;
#15268=CARTESIAN_POINT ( 'NONE',  ( 7.413471587080152858, -87.64352159168326750, -3.013058070223548324 ) ) ;
#15405=CARTESIAN_POINT ( 'NONE',  ( 9.999952458099503616, 246.0001188547612685, 0.2653554233229091230 ) ) ;
#15443=CARTESIAN_POINT ( 'NONE',  ( -7.744168461338430731, -81.53745938284842509, 2.019395720771552050 ) ) ;
#15591=CARTESIAN_POINT ( 'NONE',  ( -4.658465013329191606, -66.32363879673093265, 3.783534922165390668 ) ) ;
#15652=EDGE_CURVE ( 'NONE', #73667, #22177, #36846, .T. ) ;
#15797=CARTESIAN_POINT ( 'NONE',  ( 6.928203230275508773, -85.26883324508999351, -4.000000000000002665 ) ) ;
#15986=VERTEX_POINT ( 'NONE', #88616 ) ;
#15988=CARTESIAN_POINT ( 'NONE',  ( -9.165151389911699198, 250.2671078128291242, -4.000000000000002665 ) ) ;
#16083=CARTESIAN_POINT ( 'NONE',  ( 5.725004243152312711, -81.42480851744635117, -1.812899781754687911 ) ) ;
#16124=CARTESIAN_POINT ( 'NONE',  ( 7.151597709147948123, -66.78929265052218511, 3.587174531012141898 ) ) ;
#16126=FACE_BOUND ( 'NONE', #44145, .T. ) ;
#16219=CARTESIAN_POINT ( 'NONE',  ( -5.980543423763064581, -88.97096407501076953, -0.5500789318242851333 ) ) ;
#16226=CYLINDRICAL_SURFACE ( 'NONE', #77311, 8.000000000000000000 ) ;
#16262=ORIENTED_EDGE ( 'NONE', *, *, #27462, .F. ) ;
#16309=CARTESIAN_POINT ( 'NONE',  ( -4.472135954999579610, -85.00000000000000000, -4.000000000000001776 ) ) ;
#16323=CARTESIAN_POINT ( 'NONE',  ( 7.897196874019792645, -88.79127204167808429, -1.302055520192090032 ) ) ;
#16392=ORIENTED_EDGE ( 'NONE', *, *, #52749, .F. ) ;
#16409=ORIENTED_EDGE ( 'NONE', *, *, #85983, .F. ) ;
#16477=CARTESIAN_POINT ( 'NONE',  ( 7.211357414135266986, -7.988534600655595064, 3.467230644691329466 ) ) ;
#16510=CARTESIAN_POINT ( 'NONE',  ( -6.928203230275507885, -85.00000000000000000, -4.000000000000001776 ) ) ;
#16659=FACE_OUTER_BOUND ( 'NONE', #84846, .T. ) ;
#16679=DIRECTION ( 'NONE',  ( 0.000000000000000000, 0.000000000000000000, -1.000000000000000000 ) ) ;
#16767=MECHANICAL_DESIGN_GEOMETRIC_PRESENTATION_REPRESENTATION('',(#9914),#47780);
#16850=CARTESIAN_POINT ( 'NONE',  ( -7.002619243997878051, -66.05007318013817041, -3.868708944013001361 ) ) ;
#16896=ORIENTED_EDGE ( 'NONE', *, *, #100922, .F. ) ;
#17021=CARTESIAN_POINT ( 'NONE',  ( 6.928203230275511437, -9.734738430674132914, 4.000000000000000000 ) ) ;
#17035=CIRCLE ( 'NONE', #73836, 12.00000000000003908 ) ;
#17057=CARTESIAN_POINT ( 'NONE',  ( -7.344361273354515163, -82.55439469411474818, -3.175733139645588121 ) ) ;
#17089=EDGE_CURVE ( 'NONE', #63464, #39277, #105649, .T. ) ;
#17170=CARTESIAN_POINT ( 'NONE',  ( 5.477432325710316796, -81.83520464429525987, 2.459915882346686899 ) ) ;
#17385=LINE ( 'NONE', #19540, #89413 ) ;
#17413=CARTESIAN_POINT ( 'NONE',  ( -4.905018583967747148, 252.0235998567968352, -3.459768807258299272 ) ) ;
#17474=ORIENTED_EDGE ( 'NONE', *, *, #58343, .T. ) ;
#17558=CARTESIAN_POINT ( 'NONE',  ( 7.412906595240166041, -7.358117271477464527, 3.014362223629233561 ) ) ;
#17602=CARTESIAN_POINT ( 'NONE',  ( -9.253800200985708102, 251.3001033108817523, -3.791983798715478304 ) ) ;
#17651=CARTESIAN_POINT ( 'NONE',  ( 4.497472161260650303, -10.54222546625947388, -3.972129482042464410 ) ) ;
#17659=CARTESIAN_POINT ( 'NONE',  ( -5.725004243152317152, 246.4248085174462801, -1.812899781754681472 ) ) ;
#17732=ORIENTED_EDGE ( 'NONE', *, *, #31054, .T. ) ;
#17841=CARTESIAN_POINT ( 'NONE',  ( -5.190609988845227285, -87.63922286743591883, -3.016375611400009316 ) ) ;
#17895=CARTESIAN_POINT ( 'NONE',  ( 7.212408192734265810, -82.98482910679629754, -3.465038817813880456 ) ) ;
#17944=CARTESIAN_POINT ( 'NONE',  ( -4.904566723942681783, 252.0224270247073832, 3.460360782932705437 ) ) ;
#17992=CARTESIAN_POINT ( 'NONE',  ( -6.928203230275509661, -65.00000000000000000, -4.000000000000002665 ) ) ;
#18203=CARTESIAN_POINT ( 'NONE',  ( -4.658465013329187165, 248.6763612032690105, 3.783534922165396441 ) ) ;
#18235=CARTESIAN_POINT ( 'NONE',  ( -9.165151389911699198, 249.9999999999999716, -4.000000000000002665 ) ) ;
#18254=EDGE_LOOP ( 'NONE', ( #46891, #24957 ) ) ;
#18269=CARTESIAN_POINT ( 'NONE',  ( -7.045755811259134305, -8.696583969864475350, 3.790843699961852664 ) ) ;
#18297=CARTESIAN_POINT ( 'NONE',  ( 4.567209634097043391, 249.0640021391448045, -3.891254717191809931 ) ) ;
#18375=CARTESIAN_POINT ( 'NONE',  ( 9.165151389911699198, 250.2673515560711621, -4.000000000000002665 ) ) ;
#18476=VECTOR ( 'NONE', #32537, 1000.000000000000000 ) ;
#18483=CARTESIAN_POINT ( 'NONE',  ( -4.656390720430131580, 251.3164618596054254, 3.786082374785823212 ) ) ;
#18496=TOROIDAL_SURFACE ( 'NONE', #87396, 12.00000000000003908, 1.000000000000000000 ) ;
#18548=CARTESIAN_POINT ( 'NONE',  ( -5.981118819178463220, -6.028165438199430959, 0.5452870891823657917 ) ) ;
#18683=CARTESIAN_POINT ( 'NONE',  ( 4.813555570991629118, 251.7947379651731978, -3.584128953194764655 ) ) ;
#18715=CARTESIAN_POINT ( 'NONE',  ( 7.934914944860278041, -61.13154352799890034, -1.051261972695690217 ) ) ;
#18723=CARTESIAN_POINT ( 'NONE',  ( -5.646888413699858944, -81.55025844029613324, 2.040714635159925905 ) ) ;
#18727=EDGE_CURVE ( 'NONE', #19102, #31789, #80146, .T. ) ;
#18738=CARTESIAN_POINT ( 'NONE',  ( 5.727189096784631950, -13.57869875248741387, -1.806430436190354705 ) ) ;
#18750=CARTESIAN_POINT ( 'NONE',  ( -4.656749229489890674, 248.6823959187356365, -3.785628640239142584 ) ) ;
#18759=CARTESIAN_POINT ( 'NONE',  ( 7.414580834929599185, -87.64656280281482736, 3.010264818013836052 ) ) ;
#18819=CARTESIAN_POINT ( 'NONE',  ( -7.212994264445060644, -7.982886556599625649, 3.463766307298585811 ) ) ;
#18927=CARTESIAN_POINT ( 'NONE',  ( 9.253817200599849357, 251.2999272991685586, -3.791916801615176080 ) ) ;
#18935=DIRECTION ( 'NONE',  ( 0.000000000000000000, -1.000000000000000000, -0.000000000000000000 ) ) ;
#18958=CARTESIAN_POINT ( 'NONE',  ( 7.150931910075644105, -11.78625798522264390, -3.588457848165354402 ) ) ;
#18959=CARTESIAN_POINT ( 'NONE',  ( -7.897196874019790869, -61.20872795832194413, -1.302055520192090476 ) ) ;
#19031=CIRCLE ( 'NONE', #94770, 10.00000000000003730 ) ;
#19039=CARTESIAN_POINT ( 'NONE',  ( -5.999787407977320797, 253.9996811118444668, 0.2740427891042886976 ) ) ;
#19102=VERTEX_POINT ( 'NONE', #93868 ) ;
#19160=ORIENTED_EDGE ( 'NONE', *, *, #17089, .F. ) ;
#19238=CARTESIAN_POINT ( 'NONE',  ( 5.093234209762004916, 252.4446777346490194, 3.176141468578033145 ) ) ;
#19240=CARTESIAN_POINT ( 'NONE',  ( -4.472135954999579610, -85.00000000000000000, 4.000000000000001776 ) ) ;
#19270=EDGE_LOOP ( 'NONE', ( #54047, #40537 ) ) ;
#19275=CARTESIAN_POINT ( 'NONE',  ( 7.999912353029504430, -61.00017529396908600, -0.2691822806795002299 ) ) ;
#19283=CARTESIAN_POINT ( 'NONE',  ( -4.567209634097050497, -84.06400213914488972, -3.891254717191802381 ) ) ;
#19294=CARTESIAN_POINT ( 'NONE',  ( 5.649205854336971200, -13.45354532811516179, -2.034449005107564545 ) ) ;
#19315=LINE ( 'NONE', #43535, #45154 ) ;
#19391=CARTESIAN_POINT ( 'NONE',  ( 4.904566723942675566, 247.9775729752925315, 3.460360782932712986 ) ) ;
#19467=CARTESIAN_POINT ( 'NONE',  ( 9.333892298909278296, 251.7827573162502688, -3.590295303293472795 ) ) ;
#19540=CARTESIAN_POINT ( 'NONE',  ( 1.592040838891563829E-15, -100.0000000000000000, 13.00000000000003730 ) ) ;
#19576=CARTESIAN_POINT ( 'NONE',  ( -4.472135954999578722, 250.2707722006736049, 3.999999999999999112 ) ) ;
#19711=CARTESIAN_POINT ( 'NONE',  ( 9.797936955406328252, 246.5332831022951154, -2.012343231877608218 ) ) ;
#19793=CARTESIAN_POINT ( 'NONE',  ( 7.619701877737479201, -61.82557840467232069, -2.447562251315979154 ) ) ;
#19804=ORIENTED_EDGE ( 'NONE', *, *, #88910, .F. ) ;
#19812=CARTESIAN_POINT ( 'NONE',  ( 6.000208918519489565, -14.00031337789968333, -0.2646532170642350024 ) ) ;
#19821=CARTESIAN_POINT ( 'NONE',  ( -5.909155701201248334, -61.13738319811270827, 1.073778020691675161 ) ) ;
#19826=CARTESIAN_POINT ( 'NONE',  ( -4.815811321232733810, 248.1992329230262158, 3.581116321197045593 ) ) ;
#19859=CARTESIAN_POINT ( 'NONE',  ( -9.698972129396532083, 246.8237028725805828, -2.445345647270314782 ) ) ;
#19901=CARTESIAN_POINT ( 'NONE',  ( 7.897196874019792645, -68.79127204167807008, -1.302055520192085813 ) ) ;
#19920=CARTESIAN_POINT ( 'NONE',  ( 5.191472769733068482, 247.3590842328105168, -3.014900733016769863 ) ) ;
#19934=ORIENTED_EDGE ( 'NONE', *, *, #29209, .T. ) ;
#20031=CARTESIAN_POINT ( 'NONE',  ( 7.045755811259135193, -11.30341603013554064, 3.790843699961852664 ) ) ;
#20161=ORIENTED_EDGE ( 'NONE', *, *, #22034, .F. ) ;
#20213=VERTEX_POINT ( 'NONE', #43220 ) ;
#20263=ADVANCED_FACE ( 'NONE', ( #45357, #72659, #7382, #79689, #5798 ), #106074, .F. ) ;
#20366=CARTESIAN_POINT ( 'NONE',  ( -4.904566723942681783, -62.97757297529252440, 3.460360782932704549 ) ) ;
#20380=SURFACE_SIDE_STYLE ('',( #102835 ) ) ;
#20462=CARTESIAN_POINT ( 'NONE',  ( 5.725004243152316263, -6.424808517446342293, -1.812899781754680362 ) ) ;
#20544=CARTESIAN_POINT ( 'NONE',  ( 4.497431761510337189, -64.45901875748970156, -3.972160586670089089 ) ) ;
#20600=CARTESIAN_POINT ( 'NONE',  ( 7.551437640244095917, -81.99127537477087913, -2.648272645923386737 ) ) ;
#20622=CARTESIAN_POINT ( 'NONE',  ( -7.551437640244095917, -68.00872462522907824, -2.648272645923388513 ) ) ;
#20681=AXIS2_PLACEMENT_3D ( 'NONE', #67404, #51187, #101355 ) ;
#20691=CARTESIAN_POINT ( 'NONE',  ( 4.496882872040832702, -65.53788665489622645, 3.972797206970399397 ) ) ;
#20712=CARTESIAN_POINT ( 'NONE',  ( -5.727189096784631950, -6.421301247512601229, -1.806430436190350486 ) ) ;
#20723=CIRCLE ( 'NONE', #12025, 1.000000000000000888 ) ;
#20777=CARTESIAN_POINT ( 'NONE',  ( -5.980543423763065469, -13.97096407501078374, -0.5500789318242844672 ) ) ;
#20795=DIRECTION ( 'NONE',  ( 0.000000000000000000, 1.000000000000000000, 0.000000000000000000 ) ) ;
#20838=CARTESIAN_POINT ( 'NONE',  ( 4.589357672516666931, 251.0620603097723063, -3.865585121226750243 ) ) ;
#20909=FILL_AREA_STYLE ('',( #28443 ) ) ;
#20948=ORIENTED_EDGE ( 'NONE', *, *, #40628, .T. ) ;
#21035=VERTEX_POINT ( 'NONE', #67524 ) ;
#21087=CARTESIAN_POINT ( 'NONE',  ( 7.934996450857314976, -13.86862456472531058, -1.050865690281777010 ) ) ;
#21111=CARTESIAN_POINT ( 'NONE',  ( 7.934914944860278041, -81.13154352799891456, -1.051261972695691771 ) ) ;
#21122=CIRCLE ( 'NONE', #34885, 13.00000000000003730 ) ;
#21202=CARTESIAN_POINT ( 'NONE',  ( 5.649205854336968535, -68.45354532811516890, -2.034449005107560993 ) ) ;
#21285=CARTESIAN_POINT ( 'NONE',  ( -4.497431761510338077, -10.54098124251033042, -3.972160586670083759 ) ) ;
#21316=DIRECTION ( 'NONE',  ( 1.000000000000000000, -0.000000000000000000, -0.000000000000000000 ) ) ;
#21391=CARTESIAN_POINT ( 'NONE',  ( -7.999912353029506207, -88.99982470603094953, -0.2691822806795012846 ) ) ;
#21418=CARTESIAN_POINT ( 'NONE',  ( 6.928203230275508773, -9.730690703044611922, -4.000000000000000000 ) ) ;
#21464=SURFACE_STYLE_USAGE ( .BOTH. , #95331 ) ;
#21484=CYLINDRICAL_SURFACE ( 'NONE', #59069, 4.000000000000002665 ) ;
#21564=CARTESIAN_POINT ( 'NONE',  ( 5.725004243152315375, -61.42480851744632986, -1.812899781754685913 ) ) ;
#21604=CARTESIAN_POINT ( 'NONE',  ( -5.650483388624516046, -68.45566596850382268, 2.031129859422141415 ) ) ;
#21660=LINE ( 'NONE', #95519, #37459 ) ;
#21722=CARTESIAN_POINT ( 'NONE',  ( 4.472135954999578722, -65.00000000000000000, 4.000000000000002665 ) ) ;
#21730=EDGE_CURVE ( 'NONE', #78936, #104803, #53978, .T. ) ;
#21805=CARTESIAN_POINT ( 'NONE',  ( 7.151597709147949011, -86.78929265052215669, 3.587174531012140566 ) ) ;
#21812=CARTESIAN_POINT ( 'NONE',  ( -4.656749229489888897, -11.31760408126432083, -3.785628640239143028 ) ) ;
#21919=ORIENTED_EDGE ( 'NONE', *, *, #49730, .F. ) ;
#21992=STYLED_ITEM ( 'NONE', ( #95476 ), #102386 ) ;
#22034=EDGE_CURVE ( 'NONE', #28006, #25105, #73165, .T. ) ;
#22092=CARTESIAN_POINT ( 'NONE',  ( 4.472135954999577834, -64.86420795053444976, 4.000000000000002665 ) ) ;
#22177=VERTEX_POINT ( 'NONE', #3021 ) ;
#22241=DIRECTION ( 'NONE',  ( 1.000000000000000000, -0.000000000000000000, -0.000000000000000000 ) ) ;
#22253=CARTESIAN_POINT ( 'NONE',  ( -7.045755811259135193, -63.69658396986448423, 3.790843699961855773 ) ) ;
#22344=CARTESIAN_POINT ( 'NONE',  ( -4.472135954999583163, -10.27411850998327303, -4.000000000000000888 ) ) ;
#22525=CARTESIAN_POINT ( 'NONE',  ( 4.472135954999579610, -85.00000000000000000, -4.000000000000001776 ) ) ;
#22799=CARTESIAN_POINT ( 'NONE',  ( -4.595881407952572495, -8.933745667986775274, -3.857520671226064568 ) ) ;
#23024=FACE_OUTER_BOUND ( 'NONE', #25753, .T. ) ;
#23075=CARTESIAN_POINT ( 'NONE',  ( 0.000000000000000000, -99.99999999999997158, 0.000000000000000000 ) ) ;
#23126=CARTESIAN_POINT ( 'NONE',  ( 1.469576158976828483E-15, 3.000000000000002665, -12.00000000000003908 ) ) ;
#23149=ADVANCED_FACE ( 'NONE', ( #8731 ), #1694, .F. ) ;
#23168=( NAMED_UNIT ( * ) PLANE_ANGLE_UNIT ( ) SI_UNIT ( $, .RADIAN. ) );
#23183=CARTESIAN_POINT ( 'NONE',  ( -5.192560085536412906, -67.64305442631241760, 3.013051918867556189 ) ) ;
#23360=CARTESIAN_POINT ( 'NONE',  ( 4.497472161260645862, -85.54222546625945256, -3.972129482042464410 ) ) ;
#23442=CARTESIAN_POINT ( 'NONE',  ( -7.344505440741523117, -12.44618927298704314, -3.175463080953006223 ) ) ;
#23508=ORIENTED_EDGE ( 'NONE', *, *, #26321, .T. ) ;
#23516=AXIS2_PLACEMENT_3D ( 'NONE', #24436, #82083, #49180 ) ;
#23538=CARTESIAN_POINT ( 'NONE',  ( 7.999912353029504430, -6.000175293969080670, -0.2691822806795008405 ) ) ;
#23572=CARTESIAN_POINT ( 'NONE',  ( -7.413471587080152858, -82.35647840831671829, -3.013058070223548324 ) ) ;
#23610=CARTESIAN_POINT ( 'NONE',  ( 4.478476647430160718, -9.726479208179556579, 3.992942460563205120 ) ) ;
#23691=CARTESIAN_POINT ( 'NONE',  ( 5.192560085536415571, -62.35694557368758950, 3.013051918867554413 ) ) ;
#23703=FILL_AREA_STYLE ('',( #64156 ) ) ;
#23821=FACE_OUTER_BOUND ( 'NONE', #3364, .T. ) ;
#23829=CARTESIAN_POINT ( 'NONE',  ( -5.093234209761996922, -87.44467773464910465, 3.176141468578046023 ) ) ;
#23923=PRODUCT_DEFINITION ( 'UNKNOWN', '', #85274, #106061 ) ;
#23934=DIRECTION ( 'NONE',  ( 0.000000000000000000, 1.000000000000000000, 0.000000000000000000 ) ) ;
#24110=CARTESIAN_POINT ( 'NONE',  ( -7.045755811259133417, -83.69658396986446292, 3.790843699961855773 ) ) ;
#24190=DIRECTION ( 'NONE',  ( 0.000000000000000000, 0.000000000000000000, -1.000000000000000000 ) ) ;
#24224=CARTESIAN_POINT ( 'NONE',  ( 4.658465013329192494, -63.67636120326903892, 3.783534922165392000 ) ) ;
#24288=EDGE_CURVE ( 'NONE', #86829, #51816, #21660, .T. ) ;
#24371=ORIENTED_EDGE ( 'NONE', *, *, #85905, .T. ) ;
#24435=DIRECTION ( 'NONE',  ( 0.000000000000000000, 0.000000000000000000, 1.000000000000000000 ) ) ;
#24436=CARTESIAN_POINT ( 'NONE',  ( 0.000000000000000000, 1.000000000000000888, 0.000000000000000000 ) ) ;
#24445=EDGE_LOOP ( 'NONE', ( #93399, #106636 ) ) ;
#24592=CARTESIAN_POINT ( 'NONE',  ( 9.221216839714889701, 248.9524025183100946, 3.869414262756992517 ) ) ;
#24617=EDGE_CURVE ( 'NONE', #21035, #31964, #93889, .T. ) ;
#24628=EDGE_LOOP ( 'NONE', ( #65618, #23508, #87225, #96087 ) ) ;
#24635=CARTESIAN_POINT ( 'NONE',  ( -7.986711519608433285, -81.02638096376567489, -0.5300249774147601789 ) ) ;
#24641=CARTESIAN_POINT ( 'NONE',  ( -9.221346651730865318, 251.0483402006833842, -3.869102247876019973 ) ) ;
#24894=ORIENTED_EDGE ( 'NONE', *, *, #98891, .F. ) ;
#24900=DIRECTION ( 'NONE',  ( 1.000000000000000000, -0.000000000000000000, -0.000000000000000000 ) ) ;
#24957=ORIENTED_EDGE ( 'NONE', *, *, #37911, .T. ) ;
#25105=VERTEX_POINT ( 'NONE', #58963 ) ;
#25160=ORIENTED_EDGE ( 'NONE', *, *, #68044, .F. ) ;
#25213=ORIENTED_EDGE ( 'NONE', *, *, #70206, .F. ) ;
#25314=DIRECTION ( 'NONE',  ( 0.000000000000000000, 0.000000000000000000, -1.000000000000000000 ) ) ;
#25325=VERTEX_POINT ( 'NONE', #12506 ) ;
#25452=CARTESIAN_POINT ( 'NONE',  ( -7.150931910075641440, -63.21374201477737387, -3.588457848165359731 ) ) ;
#25494=DIRECTION ( 'NONE',  ( 1.000000000000000000, -0.000000000000000000, -0.000000000000000000 ) ) ;
#25532=CARTESIAN_POINT ( 'NONE',  ( -5.191472769733070258, 252.6409157671893979, -3.014900733016763645 ) ) ;
#25577=CARTESIAN_POINT ( 'NONE',  ( -6.928203230275509661, -10.00000000000000888, 4.000000000000000000 ) ) ;
#25648=ORIENTED_EDGE ( 'NONE', *, *, #14860, .F. ) ;
#25728=CARTESIAN_POINT ( 'NONE',  ( -9.221216839714882596, 251.0475974816896496, 3.869414262757008505 ) ) ;
#25753=EDGE_LOOP ( 'NONE', ( #40389, #12120, #78299, #82905 ) ) ;
#25780=CARTESIAN_POINT ( 'NONE',  ( 5.191144708981717315, -12.64030085521269342, 3.015512395308848070 ) ) ;
#25832=CARTESIAN_POINT ( 'NONE',  ( 5.093082057083965886, -82.55553793578430088, -3.176439207277721000 ) ) ;
#25835=CIRCLE ( 'NONE', #20681, 6.000000000000000888 ) ;
#25899=ADVANCED_FACE ( 'NONE', ( #71673 ), #54957, .F. ) ;
#25970=EDGE_LOOP ( 'NONE', ( #47562, #13565, #77232, #85430 ) ) ;
#26117=CARTESIAN_POINT ( 'NONE',  ( -6.943482370013978944, -10.52848370260726085, 3.973876482044364611 ) ) ;
#26248=CYLINDRICAL_SURFACE ( 'NONE', #89828, 4.000000000000001776 ) ;
#26257=CARTESIAN_POINT ( 'NONE',  ( -9.999952458099501840, 253.9998811452386462, 0.2653554233229243331 ) ) ;
#26309=CARTESIAN_POINT ( 'NONE',  ( 5.999787407977320797, -13.99968111184449171, 0.2740427891042958031 ) ) ;
#26321=EDGE_CURVE ( 'NONE', #87331, #28004, #11317, .T. ) ;
#26322=CARTESIAN_POINT ( 'NONE',  ( -5.192560085536403136, 247.3569455736875682, 3.013051918867572176 ) ) ;
#26355=CARTESIAN_POINT ( 'NONE',  ( -9.843039827103263306, 246.4091649749165924, -1.781495459429543793 ) ) ;
#26359=CARTESIAN_POINT ( 'NONE',  ( 5.382057749264594904, -82.00173201596055605, -2.659775980967107767 ) ) ;
#26411=CARTESIAN_POINT ( 'NONE',  ( 6.000208918519489565, 245.9996866221002279, -0.2646532170642357795 ) ) ;
#26519=CARTESIAN_POINT ( 'NONE',  ( -6.928203230275506108, -64.73116675491002070, -4.000000000000001776 ) ) ;
#26654=CARTESIAN_POINT ( 'NONE',  ( -4.472135954999580498, -9.729227799326372050, 4.000000000000000000 ) ) ;
#26656=CARTESIAN_POINT ( 'NONE',  ( 0.000000000000000000, 300.0000000000000568, 0.000000000000000000 ) ) ;
#26690=LINE ( 'NONE', #85979, #82595 ) ;
#26761=ORIENTED_EDGE ( 'NONE', *, *, #12607, .F. ) ;
#26783=CARTESIAN_POINT ( 'NONE',  ( 6.000469943554648466, 254.0007049167048478, 0.2622423038614427604 ) ) ;
#26835=CARTESIAN_POINT ( 'NONE',  ( 5.981118819178458779, -13.97183456180058947, 0.5452870891823661248 ) ) ;
#26844=VECTOR ( 'NONE', #78319, 1000.000000000000000 ) ;
#26848=CARTESIAN_POINT ( 'NONE',  ( -4.472135954999578722, 249.9999999999999432, 4.000000000000002665 ) ) ;
#26857=ORIENTED_EDGE ( 'NONE', *, *, #102723, .F. ) ;
#26932=CARTESIAN_POINT ( 'NONE',  ( -4.472135954999578722, 249.9999999999999432, -4.000000000000002665 ) ) ;
#26938=CARTESIAN_POINT ( 'NONE',  ( 5.094000037296067873, 247.5536587622877107, -3.174960020027676411 ) ) ;
#27015=CARTESIAN_POINT ( 'NONE',  ( 9.176645556628276523, 250.5273903240672837, 3.973966573947710135 ) ) ;
#27046=CARTESIAN_POINT ( 'NONE',  ( 7.151597709147947235, -11.78929265052215847, 3.587174531012139678 ) ) ;
#27125=CARTESIAN_POINT ( 'NONE',  ( -4.813668318631113330, 251.7951322982669353, 3.583991016754759062 ) ) ;
#27164=MECHANICAL_DESIGN_GEOMETRIC_PRESENTATION_REPRESENTATION('',(#21992),#73960);
#27186=CARTESIAN_POINT ( 'NONE',  ( -5.981691436642410764, -6.027309008058858275, -0.5384679144502708681 ) ) ;
#27229=FACE_OUTER_BOUND ( 'NONE', #6394, .T. ) ;
#27313=DIRECTION ( 'NONE',  ( 1.000000000000000000, -0.000000000000000000, -0.000000000000000000 ) ) ;
#27323=CARTESIAN_POINT ( 'NONE',  ( 5.384233811324318886, 253.0021709134476851, 2.655407383564598156 ) ) ;
#27356=CARTESIAN_POINT ( 'NONE',  ( 7.414346147791993857, -62.35410842337736170, -3.010818766110530120 ) ) ;
#27363=CARTESIAN_POINT ( 'NONE',  ( -4.472135954999579610, -84.72922779932639514, 4.000000000000002665 ) ) ;
#27370=DIRECTION ( 'NONE',  ( 1.000000000000000000, -0.000000000000000000, -0.000000000000000000 ) ) ;
#27374=CARTESIAN_POINT ( 'NONE',  ( 5.383284837158156755, -13.00049343515777878, 2.657356347551693698 ) ) ;
#27381=CARTESIAN_POINT ( 'NONE',  ( -4.567209634097050497, -64.06400213914488972, -3.891254717191805046 ) ) ;
#27386=CARTESIAN_POINT ( 'NONE',  ( -5.476751506168965555, 246.8364287713300484, -2.461144630687901902 ) ) ;
#27396=CARTESIAN_POINT ( 'NONE',  ( 7.801642220026312025, -88.58796826149033166, 1.787233835843583751 ) ) ;
#27400=DIRECTION ( 'NONE',  ( 0.000000000000000000, 1.000000000000000000, 0.000000000000000000 ) ) ;
#27416=CARTESIAN_POINT ( 'NONE',  ( -9.699016383038333800, 246.8236182855164600, 2.444973590251029893 ) ) ;
#27454=VERTEX_POINT ( 'NONE', #5664 ) ;
#27462=EDGE_CURVE ( 'NONE', #92577, #4111, #4080, .T. ) ;
#27468=EDGE_LOOP ( 'NONE', ( #80322, #35742, #91740, #32919 ) ) ;
#27476=CARTESIAN_POINT ( 'NONE',  ( 4.696906829037954978, 248.5600185251210519, -3.734050370377327344 ) ) ;
#27502=CARTESIAN_POINT ( 'NONE',  ( 0.000000000000000000, -99.99999999999997158, 6.000000000000000888 ) ) ;
#27546=AXIS2_PLACEMENT_3D ( 'NONE', #66417, #100905, #59956 ) ;
#27556=CARTESIAN_POINT ( 'NONE',  ( 9.333079356992124431, 251.7783308007486198, 3.592383266237774375 ) ) ;
#27579=CARTESIAN_POINT ( 'NONE',  ( 0.000000000000000000, 0.000000000000000000, 0.000000000000000000 ) ) ;
#27668=UNCERTAINTY_MEASURE_WITH_UNIT (LENGTH_MEASURE( 1.000000000000000082E-05 ), #101104, 'distance_accuracy_value', 'NONE');
#27730=CARTESIAN_POINT ( 'NONE',  ( -4.813668318631101783, -8.204867701733141061, 3.583991016754771497 ) ) ;
#27807=CARTESIAN_POINT ( 'NONE',  ( 9.165151389911699198, 249.7328921871707905, -4.000000000000001776 ) ) ;
#27890=CARTESIAN_POINT ( 'NONE',  ( 7.343637806710344051, -62.55636878099384290, 3.177475076494676198 ) ) ;
#27917=CARTESIAN_POINT ( 'NONE',  ( -5.382954851612912428, -62.00012508510553744, -2.657971597726730639 ) ) ;
#27953=DIRECTION ( 'NONE',  ( 0.000000000000000000, 0.000000000000000000, -1.000000000000000000 ) ) ;
#27978=CARTESIAN_POINT ( 'NONE',  ( -7.744329845603315832, -6.537117698465458204, -2.018701143083234673 ) ) ;
#27992=CARTESIAN_POINT ( 'NONE',  ( 7.619753052866895970, -68.17451502807172403, -2.447276542590448134 ) ) ;
#27999=DIRECTION ( 'NONE',  ( 0.000000000000000000, 0.000000000000000000, -1.000000000000000000 ) ) ;
#28004=VERTEX_POINT ( 'NONE', #85272 ) ;
#28006=VERTEX_POINT ( 'NONE', #78754 ) ;
#28080=CARTESIAN_POINT ( 'NONE',  ( 9.380894568449093640, 252.0113063311093526, -3.467341429141170384 ) ) ;
#28126=ORIENTED_EDGE ( 'NONE', *, *, #24617, .T. ) ;
#28160=CARTESIAN_POINT ( 'NONE',  ( -7.343637806710342275, -67.44363121900617841, 3.177475076494675310 ) ) ;
#28194=VECTOR ( 'NONE', #9978, 1000.000000000000000 ) ;
#28249=CARTESIAN_POINT ( 'NONE',  ( -5.383284837158154978, -6.999506564842242540, 2.657356347551693254 ) ) ;
#28301=ORIENTED_EDGE ( 'NONE', *, *, #40516, .T. ) ;
#28329=CARTESIAN_POINT ( 'NONE',  ( 0.000000000000000000, -100.0000000000000000, -10.00000000000001954 ) ) ;
#28357=B_SPLINE_CURVE_WITH_KNOTS ( 'NONE', 3,
 ( #1173, #19576, #3345, #100966, #18483, #27125, #17944, #58931, #83710, #60537, #60014, #51346, #92871, #2800, #42735, #52405, #19039, #84794, #51876, #85325, #43793, #35747, #68630, #11411, #99348, #25532, #91303, #17413, #50286, #83188, #11949, #4401, #86931, #63181, #14066, #55055 ),
 .UNSPECIFIED., .F., .F.,
 ( 4, 2, 2, 2, 2, 2, 2, 2, 2, 2, 2, 2, 2, 2, 2, 2, 2, 4 ),
 ( 0.01291936762762760545, 0.01372441420841340361, 0.01452946078919920177, 0.01533450736998499993, 0.01613955395077079635, 0.01694460053155659451, 0.01774964711234239267, 0.01855469369312819083, 0.01935974027391398899, 0.02016478685469979062, 0.02096983343548558879, 0.02177488001627139041, 0.02257992659705718858, 0.02338497317784298674, 0.02419001975862878837, 0.02459254304902168745, 0.02499506633941458306, 0.02580011292020054428 ),
 .UNSPECIFIED. ) ;
#28372=CARTESIAN_POINT ( 'NONE',  ( 5.909259836070535954, 253.8627720424205734, -1.072443315311453649 ) ) ;
#28423=CARTESIAN_POINT ( 'NONE',  ( -7.344505440741524893, -87.44618927298701294, -3.175463080953003558 ) ) ;
#28431=CARTESIAN_POINT ( 'NONE',  ( -5.190609988845228173, 247.3607771325640385, -3.016375611400006651 ) ) ;
#28443=FILL_AREA_STYLE_COLOUR ( '', #39972 ) ;
#28508=CARTESIAN_POINT ( 'NONE',  ( 7.003653396366580353, -66.05706205559678779, -3.866846144092868531 ) ) ;
#28526=CARTESIAN_POINT ( 'NONE',  ( 5.909259836070536842, -6.137227957579323601, -1.072443315311453205 ) ) ;
#28528=CARTESIAN_POINT ( 'NONE',  ( 5.910690929868576582, 246.1350409390679772, -1.065041252563917906 ) ) ;
#28610=CARTESIAN_POINT ( 'NONE',  ( 9.948561005166148163, 253.8699027374819934, -1.045755304005147490 ) ) ;
#28640=CARTESIAN_POINT ( 'NONE',  ( -4.656749229489883568, -66.31760408126432083, -3.785628640239150133 ) ) ;
#28662=CARTESIAN_POINT ( 'NONE',  ( 7.619701877737479201, -81.82557840467232779, -2.447562251315979598 ) ) ;
#28834=DIRECTION ( 'NONE',  ( -0.000000000000000000, -1.000000000000000000, -0.000000000000000000 ) ) ;
#28864=CARTESIAN_POINT ( 'NONE',  ( -4.815811321232737363, -11.80076707697374516, 3.581116321197038932 ) ) ;
#28940=ORIENTED_EDGE ( 'NONE', *, *, #52749, .T. ) ;
#28976=CARTESIAN_POINT ( 'NONE',  ( -7.801339272325196639, -88.58731471959700343, -1.788609912539668612 ) ) ;
#28982=CARTESIAN_POINT ( 'NONE',  ( -4.472135954999576057, -64.72670096487361491, -4.000000000000002665 ) ) ;
#29076=ORIENTED_EDGE ( 'NONE', *, *, #7193, .T. ) ;
#29155=CARTESIAN_POINT ( 'NONE',  ( 9.221249107921769550, 251.0482137149848256, 3.869340886054255968 ) ) ;
#29161=AXIS2_PLACEMENT_3D ( 'NONE', #1145, #58355, #2221 ) ;
#29205=CARTESIAN_POINT ( 'NONE',  ( 0.000000000000000000, -100.0000000000000000, 0.000000000000000000 ) ) ;
#29209=EDGE_CURVE ( 'NONE', #65228, #36313, #44599, .T. ) ;
#29210=CARTESIAN_POINT ( 'NONE',  ( 6.928203230275509661, -84.73473843067414180, 4.000000000000001776 ) ) ;
#29232=CARTESIAN_POINT ( 'NONE',  ( -8.000086790516059310, -69.00017358106005361, 0.2639471549312808474 ) ) ;
#29362=CARTESIAN_POINT ( 'NONE',  ( -13.00000000000003730, -10.00000000000000888, 0.000000000000000000 ) ) ;
#29479=CARTESIAN_POINT ( 'NONE',  ( -5.382954851612917757, -82.00012508510555165, -2.657971597726724866 ) ) ;
#29493=CARTESIAN_POINT ( 'NONE',  ( -7.045965687440310710, -86.30392463786033375, 3.790395326974321133 ) ) ;
#29500=CARTESIAN_POINT ( 'NONE',  ( -5.910690929868580135, -61.13504093906806247, -1.065041252563912133 ) ) ;
#29533=CARTESIAN_POINT ( 'NONE',  ( -9.176645556628276523, 249.4726096759326310, 3.973966573947711023 ) ) ;
#29669=CARTESIAN_POINT ( 'NONE',  ( 4.903871675326605839, -62.97914192698504365, -3.461400506969857016 ) ) ;
#29816=CARTESIAN_POINT ( 'NONE',  ( 4.472135954999578722, -65.00000000000000000, -4.000000000000002665 ) ) ;
#29865=CARTESIAN_POINT ( 'NONE',  ( 4.472135954999579610, -85.00000000000000000, 4.000000000000001776 ) ) ;
#29897=CARTESIAN_POINT ( 'NONE',  ( -4.503026011213026258, -10.54341862283317965, 3.965236350746919936 ) ) ;
#29920=AXIS2_PLACEMENT_3D ( 'NONE', #53073, #44453, #43913 ) ;
#30007=CARTESIAN_POINT ( 'NONE',  ( -6.943926999490791729, -85.53300992626148513, -3.973092371898547803 ) ) ;
#30082=SURFACE_STYLE_FILL_AREA ( #71565 ) ;
#30191=VECTOR ( 'NONE', #32218, 1000.000000000000000 ) ;
#30213=CARTESIAN_POINT ( 'NONE',  ( -5.911778709945830101, -68.86661839416569819, 1.058844270818174227 ) ) ;
#30330=ORIENTED_EDGE ( 'NONE', *, *, #47971, .F. ) ;
#30457=PRODUCT_DEFINITION_SHAPE ( 'NONE', 'NONE',  #23923 ) ;
#30468=CARTESIAN_POINT ( 'NONE',  ( -7.619701877737481865, -13.17442159532768287, -2.447562251315977822 ) ) ;
#30482=CARTESIAN_POINT ( 'NONE',  ( 4.478476647430158941, 250.2735207918204594, 3.992942460563207341 ) ) ;
#30554=CARTESIAN_POINT ( 'NONE',  ( -13.00000000000003730, -85.00000000000000000, 0.000000000000000000 ) ) ;
#30619=FILL_AREA_STYLE_COLOUR ( '', #79337 ) ;
#30640=CARTESIAN_POINT ( 'NONE',  ( 4.590682673078522846, -8.932082426878441339, 3.864023243754608927 ) ) ;
#30850=FACE_BOUND ( 'NONE', #18254, .T. ) ;
#30878=CARTESIAN_POINT ( 'NONE',  ( 4.814352310392310486, -66.79678594103575051, -3.583053941560743194 ) ) ;
#31001=CIRCLE ( 'NONE', #27546, 1.000000000000000888 ) ;
#31054=EDGE_CURVE ( 'NONE', #28006, #52756, #5578, .T. ) ;
#31155=DIRECTION ( 'NONE',  ( -0.000000000000000000, -1.000000000000000000, -0.000000000000000000 ) ) ;
#31235=CARTESIAN_POINT ( 'NONE',  ( 9.797174393178835518E-16, -100.0000000000000000, 8.000000000000007105 ) ) ;
#31257=CARTESIAN_POINT ( 'NONE',  ( 4.503026011213025370, -64.45658137716682745, 3.965236350746919047 ) ) ;
#31395=CARTESIAN_POINT ( 'NONE',  ( 0.000000000000000000, -100.0000000000000000, -8.000000000000000000 ) ) ;
#31428=CARTESIAN_POINT ( 'NONE',  ( -4.497472161260651191, -9.457774533740545664, -3.972129482042463522 ) ) ;
#31555=PLANE ( 'NONE',  #104346 ) ;
#31643=DIRECTION ( 'NONE',  ( 0.000000000000000000, 0.000000000000000000, -1.000000000000000000 ) ) ;
#31789=VERTEX_POINT ( 'NONE', #4612 ) ;
#31799=CARTESIAN_POINT ( 'NONE',  ( -5.384233811324312668, -68.00217091344775611, 2.655407383564612811 ) ) ;
#31964=VERTEX_POINT ( 'NONE', #105422 ) ;
#32053=AXIS2_PLACEMENT_3D ( 'NONE', #40368, #39857, #87874 ) ;
#32055=CARTESIAN_POINT ( 'NONE',  ( -7.934914944860276265, -13.86845647200111920, -1.051261972695689551 ) ) ;
#32132=EDGE_LOOP ( 'NONE', ( #1690, #37765 ) ) ;
#32154=B_SPLINE_CURVE_WITH_KNOTS ( 'NONE', 3,
 ( #61491, #70625, #20544, #13426, #53382, #38283, #29669, #95425, #85210, #11301, #4295, #63068, #21564, #46348, #5365, #52301, #77120, #36176, #69045, #38794, #15024, #54947, #64145, #47393, #5870, #23691, #47914, #48449, #46868, #24224, #106690, #96498, #31257, #80822, #22092, #40906 ),
 .UNSPECIFIED., .F., .F.,
 ( 4, 2, 2, 2, 2, 2, 2, 2, 2, 2, 2, 2, 2, 2, 2, 2, 2, 4 ),
 ( 0.000000000000000000, 0.0008074604767267247983, 0.001614920953453449597, 0.002422381430180174395, 0.003229841906906899193, 0.004037302383633624425, 0.004844762860360348790, 0.005652223337087073154, 0.006459683813813798386, 0.007267144290540523618, 0.008074604767267248850, 0.008882065243993972348, 0.009689525720720697580, 0.01049698619744742281, 0.01130444667417414631, 0.01211190715090087154, 0.01251563738926423502, 0.01291936762762759677 ),
 .UNSPECIFIED. ) ;
#32181=CARTESIAN_POINT ( 'NONE',  ( -7.744329845603314944, -81.53711769846545110, -2.018701143083234673 ) ) ;
#32186=CARTESIAN_POINT ( 'NONE',  ( -9.253500431420452088, 251.2977154991770590, 3.792688295761950101 ) ) ;
#32218=DIRECTION ( 'NONE',  ( 1.000000000000000000, -0.000000000000000000, -0.000000000000000000 ) ) ;
#32295=CARTESIAN_POINT ( 'NONE',  ( 1.530808498934196254E-15, 3.999999999999996447, -12.00000000000003908 ) ) ;
#32303=ORIENTED_EDGE ( 'NONE', *, *, #45812, .F. ) ;
#32408=EDGE_CURVE ( 'NONE', #49420, #5539, #31001, .T. ) ;
#32427=EDGE_CURVE ( 'NONE', #31964, #21035, #88458, .T. ) ;
#32440=CARTESIAN_POINT ( 'NONE',  ( -4.521127550501229386, -85.67610240527663734, 3.944701057164354818 ) ) ;
#32517=CARTESIAN_POINT ( 'NONE',  ( 5.383284837158154978, -88.00049343515779299, 2.657356347551699027 ) ) ;
#32537=DIRECTION ( 'NONE',  ( 1.000000000000000000, -0.000000000000000000, -0.000000000000000000 ) ) ;
#32636=LINE ( 'NONE', #67105, #7198 ) ;
#32692=CARTESIAN_POINT ( 'NONE',  ( 7.343637806710343163, -7.556368780993834910, 3.177475076494673978 ) ) ;
#32707=SURFACE_SIDE_STYLE ('',( #48312 ) ) ;
#32713=EDGE_LOOP ( 'NONE', ( #53728, #28940, #42944, #66601 ) ) ;
#32729=CARTESIAN_POINT ( 'NONE',  ( -7.619753052866895970, -81.82548497192826176, -2.447276542590447246 ) ) ;
#32735=CARTESIAN_POINT ( 'NONE',  ( -9.797936955406333581, 253.4667168977047709, -2.012343231877574468 ) ) ;
#32899=ORIENTED_EDGE ( 'NONE', *, *, #32408, .F. ) ;
#32919=ORIENTED_EDGE ( 'NONE', *, *, #58343, .F. ) ;
#32978=DIRECTION ( 'NONE',  ( -0.000000000000000000, -1.000000000000000000, -0.000000000000000000 ) ) ;
#32999=CARTESIAN_POINT ( 'NONE',  ( -7.934203308536663890, -61.13299659982202883, 1.057099537198546102 ) ) ;
#33049=CARTESIAN_POINT ( 'NONE',  ( 5.475947152006322760, -88.16217730109126194, 2.462898245435134470 ) ) ;
#33251=CARTESIAN_POINT ( 'NONE',  ( -7.414580834929599185, -82.35343719718518685, 3.010264818013836052 ) ) ;
#33326=EDGE_CURVE ( 'NONE', #83184, #39611, #46356, .T. ) ;
#33359=CARTESIAN_POINT ( 'NONE',  ( 5.999511540169428336, -81.00073269114568575, -0.2833228702578375335 ) ) ;
#33390=EDGE_CURVE ( 'NONE', #49420, #104803, #17385, .T. ) ;
#33499=FACE_OUTER_BOUND ( 'NONE', #69513, .T. ) ;
#33561=CARTESIAN_POINT ( 'NONE',  ( 0.000000000000000000, 3.000000000000002665, 0.000000000000000000 ) ) ;
#33640=CARTESIAN_POINT ( 'NONE',  ( -7.800703710507056243, -13.58595692657941711, 1.791736796405273058 ) ) ;
#33707=VERTEX_POINT ( 'NONE', #27502 ) ;
#33899=CARTESIAN_POINT ( 'NONE',  ( 5.980543423763064581, -81.02903592498923047, -0.5500789318242851333 ) ) ;
#33958=CARTESIAN_POINT ( 'NONE',  ( 4.589925132946512498, 248.9347398370747158, 3.864926970398271155 ) ) ;
#34041=CARTESIAN_POINT ( 'NONE',  ( -5.982126593009819970, -88.97334227892930869, 0.5333292889181888707 ) ) ;
#34063=DIRECTION ( 'NONE',  ( 0.000000000000000000, 0.000000000000000000, -1.000000000000000000 ) ) ;
#34121=CARTESIAN_POINT ( 'NONE',  ( 5.094000037296078531, -87.44634123771227507, -3.174960020027664420 ) ) ;
#34402=CARTESIAN_POINT ( 'NONE',  ( -6.000469943554647578, 245.9992950832949248, 0.2622423038614526969 ) ) ;
#34443=CARTESIAN_POINT ( 'NONE',  ( 5.384233811324310892, -81.99782908655225810, 2.655407383564611923 ) ) ;
#34469=CARTESIAN_POINT ( 'NONE',  ( -7.896254658894419798, -6.210708172458008214, 1.307282859663295493 ) ) ;
#34500=CARTESIAN_POINT ( 'NONE',  ( 5.856955515201468288, 246.2171094111913305, 1.326217528971456172 ) ) ;
#34568=( GEOMETRIC_REPRESENTATION_CONTEXT ( 3 ) GLOBAL_UNCERTAINTY_ASSIGNED_CONTEXT ( ( #41860 ) ) GLOBAL_UNIT_ASSIGNED_CONTEXT ( ( #4728, #63506, #38188 ) ) REPRESENTATION_CONTEXT ( 'NONE', 'WORKASPACE' ) );
#34577=CARTESIAN_POINT ( 'NONE',  ( -5.858881034796412202, -88.78586324002982622, 1.317748741875969687 ) ) ;
#34814=( NAMED_UNIT ( * ) PLANE_ANGLE_UNIT ( ) SI_UNIT ( $, .RADIAN. ) );
#34867=CARTESIAN_POINT ( 'NONE',  ( 4.472135954999576057, 250.2741185099831682, -4.000000000000002665 ) ) ;
#34885=AXIS2_PLACEMENT_3D ( 'NONE', #33561, #83154, #48642 ) ;
#34928=CARTESIAN_POINT ( 'NONE',  ( -5.650483388624516934, 246.5443340314961063, 2.031129859422147632 ) ) ;
#34959=CARTESIAN_POINT ( 'NONE',  ( -6.928203230275508773, -10.00000000000000711, -4.000000000000000000 ) ) ;
#34961=CARTESIAN_POINT ( 'NONE',  ( -9.176855344543007220, 249.4703957302258459, -3.973472207155925862 ) ) ;
#35000=ORIENTED_EDGE ( 'NONE', *, *, #52969, .T. ) ;
#35006=CARTESIAN_POINT ( 'NONE',  ( 7.002990960197236880, -66.05266818383458371, 3.868040364119525343 ) ) ;
#35129=CARTESIAN_POINT ( 'NONE',  ( -7.744329845603313167, -61.53711769846545820, -2.018701143083236449 ) ) ;
#35178=CARTESIAN_POINT ( 'NONE',  ( -7.344505440741524005, -67.44618927298704136, -3.175463080953004891 ) ) ;
#35267=CARTESIAN_POINT ( 'NONE',  ( -5.649205854336970312, -6.546454671884853305, -2.034449005107561437 ) ) ;
#35277=CARTESIAN_POINT ( 'NONE',  ( 0.000000000000000000, 4.000000000000003553, 0.000000000000000000 ) ) ;
#35369=EDGE_CURVE ( 'NONE', #68317, #41649, #63936, .T. ) ;
#35400=CARTESIAN_POINT ( 'NONE',  ( 5.647817967127114258, 253.4512640652878872, -2.038183545141138531 ) ) ;
#35417=DIRECTION ( 'NONE',  ( 1.000000000000000000, -0.000000000000000000, -0.000000000000000000 ) ) ;
#35439=CARTESIAN_POINT ( 'NONE',  ( -5.475947152006322760, -81.83782269890876648, 2.462898245435134470 ) ) ;
#35445=ORIENTED_EDGE ( 'NONE', *, *, #12607, .T. ) ;
#35462=CARTESIAN_POINT ( 'NONE',  ( -4.472135954999576946, 249.8642079505344498, 4.000000000000004441 ) ) ;
#35474=CARTESIAN_POINT ( 'NONE',  ( 7.002990960197232440, -86.05266818383456950, 3.868040364119523566 ) ) ;
#35492=CARTESIAN_POINT ( 'NONE',  ( -9.989435848181802413, 246.0261970747156397, -0.5278651953176011213 ) ) ;
#35536=EDGE_LOOP ( 'NONE', ( #92056, #101483, #78062, #64248 ) ) ;
#35542=CARTESIAN_POINT ( 'NONE',  ( 7.150931910075639664, -66.78625798522263324, -3.588457848165360620 ) ) ;
#35555=CARTESIAN_POINT ( 'NONE',  ( 5.190609988845229950, -7.360777132564092717, -3.016375611400007095 ) ) ;
#35558=CARTESIAN_POINT ( 'NONE',  ( 4.497472161260642309, 249.4577745337406043, -3.972129482042469739 ) ) ;
#35568=ORIENTED_EDGE ( 'NONE', *, *, #27462, .T. ) ;
#35640=CARTESIAN_POINT ( 'NONE',  ( 9.644834624769996978, 253.0089050020578156, 2.648308524638408823 ) ) ;
#35668=CARTESIAN_POINT ( 'NONE',  ( 7.046357527897574968, -11.30615650601004596, -3.789683693877206050 ) ) ;
#35721=CARTESIAN_POINT ( 'NONE',  ( -7.986539162393899716, -68.97327171057453654, -0.5321833565149920453 ) ) ;
#35742=ORIENTED_EDGE ( 'NONE', *, *, #21730, .F. ) ;
#35747=CARTESIAN_POINT ( 'NONE',  ( -5.727189096784630173, 253.5786987524874405, -1.806430436190359368 ) ) ;
#35763=COLOUR_RGB ( '', 0.08235294, 0.09019608, 0.10196078) ;
#35974=CARTESIAN_POINT ( 'NONE',  ( 7.896165657598945842, -61.21088868628029900, -1.307894402814547385 ) ) ;
#35982=CARTESIAN_POINT ( 'NONE',  ( -4.905018583967755141, -82.97640014320325008, -3.459768807258293055 ) ) ;
#35992=ADVANCED_FACE ( 'NONE', ( #73400 ), #74994, .F. ) ;
#35994=CARTESIAN_POINT ( 'NONE',  ( 5.094000037296076755, -12.44634123771225198, -3.174960020027660867 ) ) ;
#36006=CARTESIAN_POINT ( 'NONE',  ( -5.384233811324302010, 246.9978290865521444, 2.655407383564630575 ) ) ;
#36038=CARTESIAN_POINT ( 'NONE',  ( -9.536842176398165449, 247.3576463011600595, 3.014135744008184847 ) ) ;
#36117=ORIENTED_EDGE ( 'NONE', *, *, #73802, .T. ) ;
#36176=CARTESIAN_POINT ( 'NONE',  ( 6.000469943554648466, -60.99929508329501004, 0.2622423038614445368 ) ) ;
#36178=CARTESIAN_POINT ( 'NONE',  ( 9.948513602188011617, 253.8697794334385378, 1.045942665286124340 ) ) ;
#36209=CARTESIAN_POINT ( 'NONE',  ( -5.725004243152313599, -68.57519148255369146, -1.812899781754688577 ) ) ;
#36225=SURFACE_STYLE_USAGE ( .BOTH. , #85263 ) ;
#36230=CARTESIAN_POINT ( 'NONE',  ( 7.743982712349851916, -81.53786985239263174, 2.020119794285909709 ) ) ;
#36259=CARTESIAN_POINT ( 'NONE',  ( -7.412906595240166041, -67.64188272852254613, 3.014362223629234450 ) ) ;
#36291=EDGE_CURVE ( 'NONE', #15986, #102596, #61376, .T. ) ;
#36313=VERTEX_POINT ( 'NONE', #103412 ) ;
#36420=CARTESIAN_POINT ( 'NONE',  ( -5.909259836070536842, -13.86277204242069239, -1.072443315311454759 ) ) ;
#36474=CARTESIAN_POINT ( 'NONE',  ( -13.00000000000003730, 249.9999999999999432, -4.000000000000002665 ) ) ;
#36505=CARTESIAN_POINT ( 'NONE',  ( 7.150053860865848598, -63.21734546086022988, 3.590189269391292015 ) ) ;
#36512=CARTESIAN_POINT ( 'NONE',  ( -5.094000037296078531, -82.55365876228779598, -3.174960020027664420 ) ) ;
#36525=CARTESIAN_POINT ( 'NONE',  ( 5.858824175751779606, -13.78579060872359463, -1.318356988357140214 ) ) ;
#36532=CARTESIAN_POINT ( 'NONE',  ( -5.725989721596477011, -61.42322888743539977, 1.809923354557184894 ) ) ;
#36557=STYLED_ITEM ( 'NONE', ( #52141 ), #82390 ) ;
#36568=CARTESIAN_POINT ( 'NONE',  ( -9.333892298909287177, 248.2172426837495891, -3.590295303293448370 ) ) ;
#36599=CARTESIAN_POINT ( 'NONE',  ( -7.150931910075644993, -8.213742014777372091, -3.588457848165353514 ) ) ;
#36678=LINE ( 'NONE', #69540, #98036 ) ;
#36709=CARTESIAN_POINT ( 'NONE',  ( 9.482856158761293841, 252.4430711585471840, 3.177891129109649881 ) ) ;
#36740=CARTESIAN_POINT ( 'NONE',  ( 7.801777176595949825, -13.58827985812634509, -1.786991866639922266 ) ) ;
#36846=LINE ( 'NONE', #37378, #95950 ) ;
#36872=CARTESIAN_POINT ( 'NONE',  ( -5.475947152006328089, -6.837822698908765595, 2.462898245435122924 ) ) ;
#37027=CARTESIAN_POINT ( 'NONE',  ( 7.986452802927061612, -61.02690242308113966, 0.5332468218996361253 ) ) ;
#37034=CARTESIAN_POINT ( 'NONE',  ( -5.981118819178459667, -81.02816543819942297, 0.5452870891823808908 ) ) ;
#37047=CARTESIAN_POINT ( 'NONE',  ( -7.414346147791995634, -87.64589157662263119, -3.010818766110534561 ) ) ;
#37053=CARTESIAN_POINT ( 'NONE',  ( -5.094000037296077643, -62.55365876228777466, -3.174960020027664420 ) ) ;
#37150=CARTESIAN_POINT ( 'NONE',  ( 5.728413875956870349, -6.419357735466014958, 1.802282772585248827 ) ) ;
#37217=CIRCLE ( 'NONE', #64751, 10.00000000000000178 ) ;
#37231=CARTESIAN_POINT ( 'NONE',  ( 9.220915120640610141, 251.0445488643207739, -3.870126578504832437 ) ) ;
#37283=CARTESIAN_POINT ( 'NONE',  ( 7.414346147791995634, -82.35410842337736881, -3.010818766110534561 ) ) ;
#37312=CARTESIAN_POINT ( 'NONE',  ( -7.744991119775239241, -68.46438785425135620, -2.016316005557100333 ) ) ;
#37315=FACE_OUTER_BOUND ( 'NONE', #84855, .T. ) ;
#37378=CARTESIAN_POINT ( 'NONE',  ( -13.00000000000003730, 249.9999999999999432, 4.000000000000002665 ) ) ;
#37386=CARTESIAN_POINT ( 'NONE',  ( 5.092539576892241904, -67.44323467208434408, 3.177249149099056869 ) ) ;
#37459=VECTOR ( 'NONE', #11390, 1000.000000000000000 ) ;
#37509=CARTESIAN_POINT ( 'NONE',  ( -13.00000000000003730, -10.00000000000000888, 0.000000000000000000 ) ) ;
#37619=CARTESIAN_POINT ( 'NONE',  ( 7.800703710507055355, -6.414043073420603314, 1.791736796405271281 ) ) ;
#37628=CARTESIAN_POINT ( 'NONE',  ( -9.333079356992119102, 248.2216691992512381, 3.592383266237786366 ) ) ;
#37635=DIRECTION ( 'NONE',  ( -0.000000000000000000, -1.000000000000000000, -0.000000000000000000 ) ) ;
#37765=ORIENTED_EDGE ( 'NONE', *, *, #4284, .F. ) ;
#37795=CARTESIAN_POINT ( 'NONE',  ( -5.982126593009819970, -68.97334227892932290, 0.5333292889181892038 ) ) ;
#37815=FACE_OUTER_BOUND ( 'NONE', #27468, .T. ) ;
#37848=VECTOR ( 'NONE', #69343, 1000.000000000000000 ) ;
#37889=DIRECTION ( 'NONE',  ( -0.000000000000000000, -1.000000000000000000, -0.000000000000000000 ) ) ;
#37911=EDGE_CURVE ( 'NONE', #51816, #69452, #52967, .T. ) ;
#37912=CARTESIAN_POINT ( 'NONE',  ( 4.472135954999576946, -65.27329903512642773, -4.000000000000004441 ) ) ;
#37933=CARTESIAN_POINT ( 'NONE',  ( -4.814352310392310486, -8.203214058964258371, -3.583053941560742750 ) ) ;
#38003=CARTESIAN_POINT ( 'NONE',  ( -4.590682673078522846, -11.06791757312157465, 3.864023243754608039 ) ) ;
#38007=EDGE_CURVE ( 'NONE', #28004, #50935, #96674, .T. ) ;
#38036=STYLED_ITEM ( 'NONE', ( #54302 ), #70720 ) ;
#38067=ORIENTED_EDGE ( 'NONE', *, *, #33326, .F. ) ;
#38188=( NAMED_UNIT ( * ) SI_UNIT ( $, .STERADIAN. ) SOLID_ANGLE_UNIT ( ) );
#38283=CARTESIAN_POINT ( 'NONE',  ( 4.813555570991610466, -63.20526203482679506, -3.584128953194789968 ) ) ;
#38402=DIRECTION ( 'NONE',  ( 0.000000000000000000, -0.000000000000000000, 1.000000000000000000 ) ) ;
#38432=CARTESIAN_POINT ( 'NONE',  ( 5.999787407977320797, -68.99968111184449526, 0.2740427891043017983 ) ) ;
#38441=EDGE_LOOP ( 'NONE', ( #66088, #51184, #16409, #45236 ) ) ;
#38516=CARTESIAN_POINT ( 'NONE',  ( -5.650483388624515158, -13.45566596850383867, 2.031129859422142747 ) ) ;
#38536=VERTEX_POINT ( 'NONE', #100530 ) ;
#38652=CARTESIAN_POINT ( 'NONE',  ( 7.002619243997877163, -8.949926819861829586, -3.868708944012998696 ) ) ;
#38720=DIRECTION ( 'NONE',  ( -0.000000000000000000, 1.000000000000000000, -0.000000000000000000 ) ) ;
#38794=CARTESIAN_POINT ( 'NONE',  ( 5.911778709945830101, -61.13338160583428760, 1.058844270818172451 ) ) ;
#38798=VECTOR ( 'NONE', #55672, 1000.000000000000000 ) ;
#38818=CARTESIAN_POINT ( 'NONE',  ( -9.699121749566383954, 253.1766876027581930, 2.444499528233548435 ) ) ;
#38946=CARTESIAN_POINT ( 'NONE',  ( 4.660674839411963255, -66.31782485304402996, -3.778981567323764779 ) ) ;
#39004=LINE ( 'NONE', #71884, #38798 ) ;
#39018=CARTESIAN_POINT ( 'NONE',  ( 4.472135954999579610, -85.00000000000000000, 4.000000000000001776 ) ) ;
#39030=CARTESIAN_POINT ( 'NONE',  ( 7.744329845603314944, -88.46288230153457732, -2.018701143083234673 ) ) ;
#39113=CARTESIAN_POINT ( 'NONE',  ( -13.00000000000003730, 249.9999999999999432, -4.000000000000002665 ) ) ;
#39277=VERTEX_POINT ( 'NONE', #69153 ) ;
#39339=VECTOR ( 'NONE', #70414, 1000.000000000000000 ) ;
#39344=CARTESIAN_POINT ( 'NONE',  ( -13.00000000000003730, 249.9999999999999432, 0.000000000000000000 ) ) ;
#39501=CARTESIAN_POINT ( 'NONE',  ( -4.696906829037968301, -8.560018525121078525, -3.734050370377311800 ) ) ;
#39611=VERTEX_POINT ( 'NONE', #105731 ) ;
#39707=CARTESIAN_POINT ( 'NONE',  ( 7.344505440741524893, -7.553810727012976400, -3.175463080953007999 ) ) ;
#39743=CARTESIAN_POINT ( 'NONE',  ( 0.000000000000000000, 300.0000000000000568, -10.00000000000000178 ) ) ;
#39783=CARTESIAN_POINT ( 'NONE',  ( 5.384233811324309116, -6.997829086552269651, 2.655407383564615920 ) ) ;
#39857=DIRECTION ( 'NONE',  ( 0.000000000000000000, 1.000000000000000000, 0.000000000000000000 ) ) ;
#39886=FACE_OUTER_BOUND ( 'NONE', #8172, .T. ) ;
#39972=COLOUR_RGB ( '', 0.31764706, 0.68627451, 0.89019608) ;
#39984=EDGE_LOOP ( 'NONE', ( #7211, #19934 ) ) ;
#40154=ORIENTED_EDGE ( 'NONE', *, *, #61572, .F. ) ;
#40211=CARTESIAN_POINT ( 'NONE',  ( 9.948181520647876752, 246.1310719723961995, 1.049088206181493677 ) ) ;
#40270=ORIENTED_EDGE ( 'NONE', *, *, #26321, .F. ) ;
#40368=CARTESIAN_POINT ( 'NONE',  ( 0.000000000000000000, -99.99999999999997158, 0.000000000000000000 ) ) ;
#40389=ORIENTED_EDGE ( 'NONE', *, *, #93604, .F. ) ;
#40390=ORIENTED_EDGE ( 'NONE', *, *, #42885, .F. ) ;
#40510=FACE_BOUND ( 'NONE', #32132, .T. ) ;
#40516=EDGE_CURVE ( 'NONE', #50935, #4789, #8, .T. ) ;
#40537=ORIENTED_EDGE ( 'NONE', *, *, #57076, .F. ) ;
#40577=CARTESIAN_POINT ( 'NONE',  ( 5.191472769733078252, -87.64091576718952581, -3.014900733016756540 ) ) ;
#40604=DIRECTION ( 'NONE',  ( 0.000000000000000000, 0.000000000000000000, 1.000000000000000000 ) ) ;
#40628=EDGE_CURVE ( 'NONE', #104803, #39277, #101475, .T. ) ;
#40722=CIRCLE ( 'NONE', #23516, 13.00000000000003730 ) ;
#40761=FILL_AREA_STYLE_COLOUR ( '', #35763 ) ;
#40781=CARTESIAN_POINT ( 'NONE',  ( -7.213352437320217803, -82.98163526992318850, -3.463014597543483841 ) ) ;
#40906=CARTESIAN_POINT ( 'NONE',  ( 4.472135954999578722, -65.00000000000000000, 4.000000000000002665 ) ) ;
#41038=CARTESIAN_POINT ( 'NONE',  ( -4.658465013329192494, -86.32363879673094686, 3.783534922165390668 ) ) ;
#41310=ORIENTED_EDGE ( 'NONE', *, *, #56018, .F. ) ;
#41322=CARTESIAN_POINT ( 'NONE',  ( -9.482945380845308136, 252.4433305877892337, 3.177595346755267336 ) ) ;
#41565=CARTESIAN_POINT ( 'NONE',  ( -4.813555570991609578, -86.79473796517322626, -3.584128953194789968 ) ) ;
#41643=CARTESIAN_POINT ( 'NONE',  ( 5.999787407977321685, -88.99968111184452368, 0.2740427891043037412 ) ) ;
#41649=VERTEX_POINT ( 'NONE', #58599 ) ;
#41716=CARTESIAN_POINT ( 'NONE',  ( -7.150053860865849487, -11.78265453913977545, 3.590189269391290683 ) ) ;
#41802=CARTESIAN_POINT ( 'NONE',  ( 9.253500431420448535, 248.7022845008229126, 3.792688295761959871 ) ) ;
#41852=CARTESIAN_POINT ( 'NONE',  ( -10.00004721872061353, 254.0001180468113944, -0.2617599822266347687 ) ) ;
#41860=UNCERTAINTY_MEASURE_WITH_UNIT (LENGTH_MEASURE( 1.000000000000000082E-05 ), #4728, 'distance_accuracy_value', 'NONE');
#42089=CARTESIAN_POINT ( 'NONE',  ( -5.911778709945830101, -88.86661839416575503, 1.058844270818174227 ) ) ;
#42167=CARTESIAN_POINT ( 'NONE',  ( 5.910690929868580135, -88.86495906093198016, -1.065041252563905028 ) ) ;
#42297=LINE ( 'NONE', #76259, #97694 ) ;
#42318=VECTOR ( 'NONE', #101657, 1000.000000000000000 ) ;
#42383=CARTESIAN_POINT ( 'NONE',  ( -9.381394091586582107, 252.0134960558159776, 3.465950112474283085 ) ) ;
#42437=CARTESIAN_POINT ( 'NONE',  ( 5.477578620271508214, -13.16501439016104236, -2.459398706554656755 ) ) ;
#42445=CARTESIAN_POINT ( 'NONE',  ( 1.224646799147354440E-15, 300.0000000000000568, 10.00000000000000178 ) ) ;
#42448=CARTESIAN_POINT ( 'NONE',  ( -5.382057749264597568, 247.0017320159604992, -2.659775980967104658 ) ) ;
#42511=CARTESIAN_POINT ( 'NONE',  ( -7.986468734911285949, -6.026863202769209060, 0.5341897780976081478 ) ) ;
#42622=CARTESIAN_POINT ( 'NONE',  ( -5.725004243152312711, -88.57519148255366304, -1.812899781754687911 ) ) ;
#42707=AXIS2_PLACEMENT_3D ( 'NONE', #87721, #102837, #13803 ) ;
#42735=CARTESIAN_POINT ( 'NONE',  ( -5.909155701201250110, 253.8626168018873273, 1.073778020691660062 ) ) ;
#42885=EDGE_CURVE ( 'NONE', #39611, #83184, #87571, .T. ) ;
#42913=EDGE_LOOP ( 'NONE', ( #78833, #98637, #65489, #45636 ) ) ;
#42927=CARTESIAN_POINT ( 'NONE',  ( 5.476751506168977102, 253.1635712286698947, -2.461144630687876145 ) ) ;
#42944=ORIENTED_EDGE ( 'NONE', *, *, #45812, .T. ) ;
#42994=CARTESIAN_POINT ( 'NONE',  ( -5.980543423763066357, 246.0290359249892163, -0.5500789318242816917 ) ) ;
#43030=CARTESIAN_POINT ( 'NONE',  ( 4.815811321232738251, -83.19923292302624418, 3.581116321197038044 ) ) ;
#43059=CARTESIAN_POINT ( 'NONE',  ( -7.344133061198930612, -7.555056073194249322, 3.176267128233874804 ) ) ;
#43067=ORIENTED_EDGE ( 'NONE', *, *, #43375, .F. ) ;
#43136=ORIENTED_EDGE ( 'NONE', *, *, #66593, .F. ) ;
#43164=CARTESIAN_POINT ( 'NONE',  ( 9.165151389911699198, 249.9999999999999432, 4.000000000000002665 ) ) ;
#43191=CARTESIAN_POINT ( 'NONE',  ( -6.928203230275508773, -85.00000000000000000, 4.000000000000001776 ) ) ;
#43220=CARTESIAN_POINT ( 'NONE',  ( 7.347880794884120722E-16, 299.9999999999999432, -6.000000000000000888 ) ) ;
#43246=CARTESIAN_POINT ( 'NONE',  ( -7.896571385775231100, -68.78997999345754977, 1.305932416347435954 ) ) ;
#43337=DIRECTION ( 'NONE',  ( 0.000000000000000000, 0.000000000000000000, -1.000000000000000000 ) ) ;
#43375=EDGE_CURVE ( 'NONE', #5539, #57603, #17035, .T. ) ;
#43406=SURFACE_STYLE_FILL_AREA ( #99489 ) ;
#43464=CARTESIAN_POINT ( 'NONE',  ( 5.999511540169428336, 253.9992673088543143, -0.2833228702578392544 ) ) ;
#43512=CARTESIAN_POINT ( 'NONE',  ( 5.725989721596482340, -13.57677111256461622, 1.809923354557178898 ) ) ;
#43528=EDGE_LOOP ( 'NONE', ( #60104, #9227, #24371, #86384 ) ) ;
#43535=CARTESIAN_POINT ( 'NONE',  ( -13.00000000000003730, -10.00000000000000888, -4.000000000000000000 ) ) ;
#43580=CARTESIAN_POINT ( 'NONE',  ( -7.551892080562054410, -6.990122974606172157, 2.647003822403975359 ) ) ;
#43606=CARTESIAN_POINT ( 'NONE',  ( 4.472135954999582275, -9.725881490016750064, -4.000000000000000000 ) ) ;
#43608=CARTESIAN_POINT ( 'NONE',  ( 5.909155701201248334, 246.1373831981126727, 1.073778020691680490 ) ) ;
#43717=CARTESIAN_POINT ( 'NONE',  ( 7.986711519608431509, -13.97361903623434820, -0.5300249774147621773 ) ) ;
#43767=ADVANCED_FACE ( 'NONE', ( #46988 ), #12493, .T. ) ;
#43768=CARTESIAN_POINT ( 'NONE',  ( -7.934914944860276265, -68.86845647200111387, -1.051261972695694213 ) ) ;
#43793=CARTESIAN_POINT ( 'NONE',  ( -5.858824175751776941, 253.7857906087234028, -1.318356988357146431 ) ) ;
#43863=DIRECTION ( 'NONE',  ( -0.000000000000000000, -1.000000000000000000, -0.000000000000000000 ) ) ;
#43913=DIRECTION ( 'NONE',  ( 0.000000000000000000, 0.000000000000000000, -1.000000000000000000 ) ) ;
#43989=CARTESIAN_POINT ( 'NONE',  ( 5.982126593009819970, 253.9733422789293229, 0.5333292889181895369 ) ) ;
#44021=CARTESIAN_POINT ( 'NONE',  ( 7.743982712349851916, -61.53786985239262464, 2.020119794285911041 ) ) ;
#44055=CARTESIAN_POINT ( 'NONE',  ( -5.982126593009819082, 246.0266577210706203, 0.5333292889181968643 ) ) ;
#44090=DIRECTION ( 'NONE',  ( -0.000000000000000000, -1.000000000000000000, -0.000000000000000000 ) ) ;
#44123=CARTESIAN_POINT ( 'NONE',  ( -6.928203230275508773, -10.00000000000000711, -4.000000000000000000 ) ) ;
#44138=CARTESIAN_POINT ( 'NONE',  ( 7.213352437320218691, -67.01836473007682571, -3.463014597543476736 ) ) ;
#44145=EDGE_LOOP ( 'NONE', ( #28301, #69668 ) ) ;
#44148=CARTESIAN_POINT ( 'NONE',  ( 5.647817967127100047, -6.548735934712071050, -2.038183545141170061 ) ) ;
#44151=CARTESIAN_POINT ( 'NONE',  ( 4.472135954999577834, 249.7267009648735439, -4.000000000000003553 ) ) ;
#44231=CARTESIAN_POINT ( 'NONE',  ( 10.00005432054558696, 254.0001358013791446, 0.2621623937322634657 ) ) ;
#44261=CARTESIAN_POINT ( 'NONE',  ( -4.589357672516644726, -66.06206030977220678, -3.865585121226772447 ) ) ;
#44432=CARTESIAN_POINT ( 'NONE',  ( 1.592040838891563829E-15, 3.000000000000002665, 13.00000000000003730 ) ) ;
#44453=DIRECTION ( 'NONE',  ( 0.000000000000000000, 1.000000000000000000, 0.000000000000000000 ) ) ;
#44521=CARTESIAN_POINT ( 'NONE',  ( -13.00000000000003730, -85.00000000000000000, 4.000000000000001776 ) ) ;
#44533=CARTESIAN_POINT ( 'NONE',  ( 5.382057749264600233, 252.9982679840394155, -2.659775980967101106 ) ) ;
#44568=CARTESIAN_POINT ( 'NONE',  ( 6.928203230275507885, -65.00000000000000000, 4.000000000000002665 ) ) ;
#44574=CARTESIAN_POINT ( 'NONE',  ( -4.656390720430120034, -83.68353814039454619, 3.786082374785836535 ) ) ;
#44593=CARTESIAN_POINT ( 'NONE',  ( -4.472135954999578722, -64.72922779932635251, 4.000000000000002665 ) ) ;
#44599=B_SPLINE_CURVE_WITH_KNOTS ( 'NONE', 3,
 ( #45472, #26654, #77297, #69221, #101031, #27730, #101571, #102089, #69739, #28249, #36872, #102633, #61671, #53019, #60076, #18548, #51412, #94561, #27186, #12014, #10422, #20712, #35267, #12537, #78344, #92940, #51940, #84854, #37933, #39501, #88047, #22799, #47029, #31428, #47561, #70268 ),
 .UNSPECIFIED., .F., .F.,
 ( 4, 2, 2, 2, 2, 2, 2, 2, 2, 2, 2, 2, 2, 2, 2, 2, 2, 4 ),
 ( 0.01291936762762758636, 0.01372441420841339493, 0.01452946078919920177, 0.01533450736998501034, 0.01613955395077081717, 0.01694460053155662574, 0.01774964711234243431, 0.01855469369312823941, 0.01935974027391405144, 0.02016478685469985654, 0.02096983343548566164, 0.02177488001627147368, 0.02257992659705727878, 0.02338497317784308735, 0.02419001975862889592, 0.02459254304902180194, 0.02499506633941470449, 0.02580011292020050959 ),
 .UNSPECIFIED. ) ;
#44664=CARTESIAN_POINT ( 'NONE',  ( -7.934203308536662114, -6.132996599822035044, 1.057099537198544326 ) ) ;
#44677=CARTESIAN_POINT ( 'NONE',  ( 7.999885325681428405, -68.99977065129940001, 0.2682325777720065973 ) ) ;
#44721=CARTESIAN_POINT ( 'NONE',  ( 0.000000000000000000, 0.000000000000000000, -12.00000000000003908 ) ) ;
#44737=ADVANCED_FACE ( 'NONE', ( #33499, #57207, #99255, #40510 ), #16226, .T. ) ;
#44772=CARTESIAN_POINT ( 'NONE',  ( 9.699016383038332023, 253.1763817144832558, 2.444973590251036555 ) ) ;
#44803=CARTESIAN_POINT ( 'NONE',  ( -5.093082057083964109, -67.44446206421571333, -3.176439207277722332 ) ) ;
#44855=EDGE_LOOP ( 'NONE', ( #56965, #54144, #35445, #26857 ) ) ;
#45014=B_SPLINE_CURVE_WITH_KNOTS ( 'NONE', 3,
 ( #74211, #49942, #73681, #25728, #32186, #50464, #42383, #41322, #71683, #90413, #38818, #59120, #99552, #58586, #106039, #48865, #26257, #41852, #91487, #65069, #56959, #92001, #32735, #290, #83374, #65602, #821, #106583, #97965, #17602, #24641, #8421, #15988, #9471 ),
 .UNSPECIFIED., .F., .F.,
 ( 4, 2, 2, 2, 2, 2, 2, 2, 2, 2, 2, 2, 2, 2, 2, 2, 4 ),
 ( 0.01263889472610567853, 0.01342810546992895433, 0.01421731621375223013, 0.01500652695757550767, 0.01579573770139878347, 0.01658494844522205927, 0.01737415918904533507, 0.01816336993286861434, 0.01895258067669189014, 0.01974179142051516594, 0.02053100216433844522, 0.02132021290816171755, 0.02210942365198499682, 0.02289863439580826915, 0.02368784513963154842, 0.02447705588345482422, 0.02526626662727810002 ),
 .UNSPECIFIED. ) ;
#45017=CARTESIAN_POINT ( 'NONE',  ( -4.472135954999581386, -10.00000000000000888, -4.000000000000000000 ) ) ;
#45103=CARTESIAN_POINT ( 'NONE',  ( 7.551437640244097693, -61.99127537477090755, -2.648272645923382740 ) ) ;
#45124=CARTESIAN_POINT ( 'NONE',  ( -7.934914944860278041, -88.86845647200112808, -1.051261972695691771 ) ) ;
#45154=VECTOR ( 'NONE', #86145, 1000.000000000000000 ) ;
#45211=CARTESIAN_POINT ( 'NONE',  ( 7.934203308536663890, -68.86700340017799249, 1.057099537198552097 ) ) ;
#45223=CARTESIAN_POINT ( 'NONE',  ( 5.093082057083966774, -7.555537935784294667, -3.176439207277719667 ) ) ;
#45236=ORIENTED_EDGE ( 'NONE', *, *, #85200, .F. ) ;
#45303=DIRECTION ( 'NONE',  ( -1.224646799147351482E-16, 0.000000000000000000, -1.000000000000000000 ) ) ;
#45331=CARTESIAN_POINT ( 'NONE',  ( 6.944031699373470090, -10.53460654556130116, 3.972913591453822502 ) ) ;
#45355=CARTESIAN_POINT ( 'NONE',  ( 7.045965687440310710, -83.69607536213965204, 3.790395326974321133 ) ) ;
#45357=FACE_OUTER_BOUND ( 'NONE', #42913, .T. ) ;
#45464=VERTEX_POINT ( 'NONE', #39743 ) ;
#45472=CARTESIAN_POINT ( 'NONE',  ( -4.472135954999580498, -10.00000000000000888, 4.000000000000000000 ) ) ;
#45542=CARTESIAN_POINT ( 'NONE',  ( -4.905194654929171172, -12.02394395019843465, 3.459476078998854565 ) ) ;
#45586=DIRECTION ( 'NONE',  ( -0.000000000000000000, -1.000000000000000000, -0.000000000000000000 ) ) ;
#45633=CARTESIAN_POINT ( 'NONE',  ( -4.472135954999579610, -85.00000000000000000, 4.000000000000001776 ) ) ;
#45636=ORIENTED_EDGE ( 'NONE', *, *, #51349, .T. ) ;
#45644=CARTESIAN_POINT ( 'NONE',  ( -7.618844049274129837, -88.17235898929459381, 2.450177051822847840 ) ) ;
#45676=CARTESIAN_POINT ( 'NONE',  ( 7.801339272325197527, -6.412685280403009891, -1.788609912539670832 ) ) ;
#45688=CARTESIAN_POINT ( 'NONE',  ( 0.000000000000000000, 0.000000000000000000, 0.000000000000000000 ) ) ;
#45708=FACE_OUTER_BOUND ( 'NONE', #35536, .T. ) ;
#45722=CARTESIAN_POINT ( 'NONE',  ( 6.944371705245972137, -65.53899691424550156, -3.972324460300565185 ) ) ;
#45731=CARTESIAN_POINT ( 'NONE',  ( -13.00000000000003730, 249.9999999999999432, 0.000000000000000000 ) ) ;
#45812=EDGE_CURVE ( 'NONE', #25325, #53932, #93611, .T. ) ;
#45871=CARTESIAN_POINT ( 'NONE',  ( 7.343637806710343163, -82.55636878099383580, 3.177475076494674866 ) ) ;
#45907=DIRECTION ( 'NONE',  ( 1.000000000000000000, -0.000000000000000000, -0.000000000000000000 ) ) ;
#45976=CARTESIAN_POINT ( 'NONE',  ( 4.595881407952571607, -66.06625433201323006, -3.857520671226067233 ) ) ;
#46065=CARTESIAN_POINT ( 'NONE',  ( -5.647817967127100935, -13.45126406528794938, -2.038183545141171393 ) ) ;
#46080=LINE ( 'NONE', #28329, #42318 ) ;
#46101=ORIENTED_EDGE ( 'NONE', *, *, #32408, .T. ) ;
#46107=CARTESIAN_POINT ( 'NONE',  ( -7.046289519167718396, -11.30591819944378074, -3.789821819998817176 ) ) ;
#46172=CARTESIAN_POINT ( 'NONE',  ( -7.412906595240168706, -87.64188272852256034, 3.014362223629233561 ) ) ;
#46205=CARTESIAN_POINT ( 'NONE',  ( 7.046289519167717508, -8.694081800556235251, -3.789821819998816288 ) ) ;
#46277=ORIENTED_EDGE ( 'NONE', *, *, #13896, .F. ) ;
#46307=B_SPLINE_CURVE_WITH_KNOTS ( 'NONE', 3,
 ( #51139, #10158, #2058, #35006, #67873, #16124, #49008, #81909, #8025, #65749, #57628, #93213, #94824, #52208, #45211, #69476, #44677, #85666, #12281, #102361, #19901, #11205, #12808, #27992, #76484, #59798, #10679, #44138, #35542, #78085, #28508, #45722, #77564, #61391 ),
 .UNSPECIFIED., .F., .F.,
 ( 4, 2, 2, 2, 2, 2, 2, 2, 2, 2, 2, 2, 2, 2, 2, 2, 4 ),
 ( 0.01272238763756222690, 0.01351613129786394599, 0.01430987495816566507, 0.01510361861846738415, 0.01589736227876910324, 0.01669110593907082232, 0.01748484959937254141, 0.01827859325967426049, 0.01907233691997597957, 0.01986608058027769866, 0.02065982424057941774, 0.02145356790088113683, 0.02224731156118285591, 0.02304105522148457846, 0.02383479888178629408, 0.02462854254208801663, 0.02542228620238973225 ),
 .UNSPECIFIED. ) ;
#46327=CARTESIAN_POINT ( 'NONE',  ( 9.165151389911699198, 249.9999999999999432, 4.000000000000002665 ) ) ;
#46348=CARTESIAN_POINT ( 'NONE',  ( 5.855777637195783036, -61.21893503241554413, -1.331220292256679372 ) ) ;
#46356=CIRCLE ( 'NONE', #29161, 8.000000000000007105 ) ;
#46399=( LENGTH_UNIT ( ) NAMED_UNIT ( * ) SI_UNIT ( .MILLI., .METRE. ) );
#46474=CARTESIAN_POINT ( 'NONE',  ( 0.000000000000000000, -100.0000000000000000, 0.000000000000000000 ) ) ;
#46575=CARTESIAN_POINT ( 'NONE',  ( 6.944031699373470090, -85.53460654556131715, 3.972913591453824278 ) ) ;
#46643=FACE_BOUND ( 'NONE', #69781, .T. ) ;
#46676=CARTESIAN_POINT ( 'NONE',  ( -4.472135954999578722, -65.00000000000000000, 4.000000000000002665 ) ) ;
#46694=CIRCLE ( 'NONE', #77729, 1.000000000000000888 ) ;
#46868=CARTESIAN_POINT ( 'NONE',  ( 4.815811321232738251, -63.19923292302625839, 3.581116321197038932 ) ) ;
#46891=ORIENTED_EDGE ( 'NONE', *, *, #70206, .T. ) ;
#46988=FACE_OUTER_BOUND ( 'NONE', #44855, .T. ) ;
#47013=CARTESIAN_POINT ( 'NONE',  ( 4.696906829037970077, -66.43998147487890549, -3.734050370377312245 ) ) ;
#47029=CARTESIAN_POINT ( 'NONE',  ( -4.567209634097053161, -9.064002139144887948, -3.891254717191801493 ) ) ;
#47030=EDGE_LOOP ( 'NONE', ( #58164, #458, #46277, #49841 ) ) ;
#47252=CARTESIAN_POINT ( 'NONE',  ( 0.000000000000000000, 1.000000000000000888, -13.00000000000003730 ) ) ;
#47284=CYLINDRICAL_SURFACE ( 'NONE', #2920, 4.000000000000002665 ) ;
#47315=DIRECTION ( 'NONE',  ( -1.000000000000000000, 0.000000000000000000, 0.000000000000000000 ) ) ;
#47393=CARTESIAN_POINT ( 'NONE',  ( 5.477432325710315020, -61.83520464429526697, 2.459915882346687344 ) ) ;
#47408=SURFACE_SIDE_STYLE ('',( #14494 ) ) ;
#47440=FACE_BOUND ( 'NONE', #87181, .T. ) ;
#47516=DIRECTION ( 'NONE',  ( 0.000000000000000000, 1.000000000000000000, 0.000000000000000000 ) ) ;
#47542=CARTESIAN_POINT ( 'NONE',  ( 5.094000037296075867, -67.44634123771224665, -3.174960020027664420 ) ) ;
#47561=CARTESIAN_POINT ( 'NONE',  ( -4.472135954999583163, -9.726700964873602473, -4.000000000000001776 ) ) ;
#47562=ORIENTED_EDGE ( 'NONE', *, *, #33390, .F. ) ;
#47613=LINE ( 'NONE', #63832, #18476 ) ;
#47777=CARTESIAN_POINT ( 'NONE',  ( -13.00000000000003730, -10.00000000000000888, 0.000000000000000000 ) ) ;
#47780=( GEOMETRIC_REPRESENTATION_CONTEXT ( 3 ) GLOBAL_UNCERTAINTY_ASSIGNED_CONTEXT ( ( #11440 ) ) GLOBAL_UNIT_ASSIGNED_CONTEXT ( ( #73649, #72599, #97393 ) ) REPRESENTATION_CONTEXT ( 'NONE', 'WORKASPACE' ) );
#47878=DIRECTION ( 'NONE',  ( 1.000000000000000000, 0.000000000000000000, 0.000000000000000000 ) ) ;
#47914=CARTESIAN_POINT ( 'NONE',  ( 5.093234209761996034, -62.55532226535091667, 3.176141468578046023 ) ) ;
#47946=CARTESIAN_POINT ( 'NONE',  ( -4.590682673078522846, -66.06791757312157642, 3.864023243754608927 ) ) ;
#47971=EDGE_CURVE ( 'NONE', #33707, #27454, #49311, .T. ) ;
#48092=DIRECTION ( 'NONE',  ( 0.000000000000000000, 0.000000000000000000, 1.000000000000000000 ) ) ;
#48151=CARTESIAN_POINT ( 'NONE',  ( 7.213352437320217803, -87.01836473007681150, -3.463014597543483841 ) ) ;
#48161=EDGE_CURVE ( 'NONE', #76918, #20213, #42297, .T. ) ;
#48162=B_SPLINE_CURVE_WITH_KNOTS ( 'NONE', 3,
 ( #46327, #5342, #8902, #24592, #41802, #246, #72579, #74690, #105481, #57439, #97377, #64509, #105996, #56375, #40211, #89310, #15405, #48292, #50414, #93564, #92478, #11552, #19711, #60157, #93020, #69296, #2406, #84933, #91441, #2936, #68218, #101650, #27807, #1321 ),
 .UNSPECIFIED., .F., .F.,
 ( 4, 2, 2, 2, 2, 2, 2, 2, 2, 2, 2, 2, 2, 2, 2, 2, 4 ),
 ( 0.01263889472610568200, 0.01342810546992895954, 0.01421731621375223881, 0.01500652695757551634, 0.01579573770139879388, 0.01658494844522207315, 0.01737415918904534895, 0.01816336993286862822, 0.01895258067669190749, 0.01974179142051518676, 0.02053100216433846603, 0.02132021290816174183, 0.02210942365198502110, 0.02289863439580829690, 0.02368784513963157617, 0.02447705588345485544, 0.02526626662727813125 ),
 .UNSPECIFIED. ) ;
#48239=ADVANCED_FACE ( 'NONE', ( #27229, #67653 ), #86518, .T. ) ;
#48292=CARTESIAN_POINT ( 'NONE',  ( 10.00004721872061531, 245.9998819531884635, -0.2617599822266503118 ) ) ;
#48312=SURFACE_STYLE_FILL_AREA ( #80157 ) ;
#48422=DIRECTION ( 'NONE',  ( 1.000000000000000000, -0.000000000000000000, 1.224646799147353207E-16 ) ) ;
#48449=CARTESIAN_POINT ( 'NONE',  ( 4.905194654929172948, -62.97605604980157068, 3.459476078998854121 ) ) ;
#48482=CARTESIAN_POINT ( 'NONE',  ( -4.472135954999577834, -65.13579204946555024, 4.000000000000002665 ) ) ;
#48485=FACE_BOUND ( 'NONE', #83545, .T. ) ;
#48493=ORIENTED_EDGE ( 'NONE', *, *, #769, .F. ) ;
#48517=EDGE_LOOP ( 'NONE', ( #60426, #48493 ) ) ;
#48578=CARTESIAN_POINT ( 'NONE',  ( -4.815811321232738251, -86.80076707697375582, 3.581116321197038044 ) ) ;
#48642=DIRECTION ( 'NONE',  ( 0.000000000000000000, 0.000000000000000000, 1.000000000000000000 ) ) ;
#48649=CARTESIAN_POINT ( 'NONE',  ( 5.646888413699858944, -88.44974155970389518, 2.040714635159925905 ) ) ;
#48755=EDGE_CURVE ( 'NONE', #52756, #28006, #104602, .T. ) ;
#48756=ORIENTED_EDGE ( 'NONE', *, *, #18727, .F. ) ;
#48782=EDGE_CURVE ( 'NONE', #78936, #63464, #20723, .T. ) ;
#48865=CARTESIAN_POINT ( 'NONE',  ( -9.989113211954183669, 253.9729927354898393, 0.5334031035449283698 ) ) ;
#48909=AXIS2_PLACEMENT_3D ( 'NONE', #61322, #96343, #103362 ) ;
#48963=CARTESIAN_POINT ( 'NONE',  ( 5.982126593009819970, -81.02665772107070552, 0.5333292889181888707 ) ) ;
#49008=CARTESIAN_POINT ( 'NONE',  ( 7.212994264445059756, -67.01711344340039034, 3.463766307298588920 ) ) ;
#49055=EDGE_CURVE ( 'NONE', #31789, #67191, #94313, .T. ) ;
#49106=CARTESIAN_POINT ( 'NONE',  ( -4.478476647430158941, -85.27352079182048783, 3.992942460563208229 ) ) ;
#49132=DIRECTION ( 'NONE',  ( 0.000000000000000000, 0.000000000000000000, -1.000000000000000000 ) ) ;
#49176=CARTESIAN_POINT ( 'NONE',  ( -13.00000000000003730, 249.9999999999999432, 0.000000000000000000 ) ) ;
#49180=DIRECTION ( 'NONE',  ( 0.000000000000000000, 0.000000000000000000, -1.000000000000000000 ) ) ;
#49214=CARTESIAN_POINT ( 'NONE',  ( 6.928203230275507885, -85.00000000000000000, -4.000000000000001776 ) ) ;
#49221=ORIENTED_EDGE ( 'NONE', *, *, #55180, .T. ) ;
#49260=CARTESIAN_POINT ( 'NONE',  ( -7.896571385775229324, -13.78997999345754444, 1.305932416347439284 ) ) ;
#49311=LINE ( 'NONE', #72020, #8840 ) ;
#49420=VERTEX_POINT ( 'NONE', #44432 ) ;
#49513=DIRECTION ( 'NONE',  ( 0.000000000000000000, 0.000000000000000000, -1.000000000000000000 ) ) ;
#49649=CARTESIAN_POINT ( 'NONE',  ( -4.472135954999578722, -85.27411850998325349, -4.000000000000003553 ) ) ;
#49730=EDGE_CURVE ( 'NONE', #101817, #84992, #87813, .T. ) ;
#49799=CARTESIAN_POINT ( 'NONE',  ( -7.618844049274132502, -13.17235898929460802, 2.450177051822845620 ) ) ;
#49841=ORIENTED_EDGE ( 'NONE', *, *, #82355, .F. ) ;
#49936=CARTESIAN_POINT ( 'NONE',  ( -7.003653396366579464, -83.94293794440324064, -3.866846144092870308 ) ) ;
#49942=CARTESIAN_POINT ( 'NONE',  ( -9.165151389911704527, 250.2629551091633573, 4.000000000000000888 ) ) ;
#50041=CARTESIAN_POINT ( 'NONE',  ( 4.478476647430158941, -84.72647920817956901, 3.992942460563208229 ) ) ;
#50184=CARTESIAN_POINT ( 'NONE',  ( -4.472135954999579610, -85.00000000000000000, -4.000000000000001776 ) ) ;
#50211=CARTESIAN_POINT ( 'NONE',  ( -7.619753052866895082, -61.82548497192825465, -2.447276542590449910 ) ) ;
#50286=CARTESIAN_POINT ( 'NONE',  ( -4.814352310392307821, 251.7967859410357221, -3.583053941560747191 ) ) ;
#50289=EDGE_LOOP ( 'NONE', ( #72841, #55916, #40390, #85741 ) ) ;
#50414=CARTESIAN_POINT ( 'NONE',  ( 9.989690267985817940, 246.0255558340508628, -0.5238310916885806634 ) ) ;
#50423=CARTESIAN_POINT ( 'NONE',  ( -13.00000000000003730, -65.00000000000000000, -4.000000000000002665 ) ) ;
#50433=B_SPLINE_CURVE_WITH_KNOTS ( 'NONE', 3,
 ( #66287, #74891, #58194, #33958, #66829, #69491, #19391, #2070, #61409, #67886, #93763, #59277, #2608, #34500, #43608, #100246, #85134, #26411, #76500, #28528, #94300, #9629, #52223, #60874, #93229, #19920, #26938, #101843, #10694, #27476, #59811, #11224, #18297, #35558, #44151, #92152 ),
 .UNSPECIFIED., .F., .F.,
 ( 4, 2, 2, 2, 2, 2, 2, 2, 2, 2, 2, 2, 2, 2, 2, 2, 2, 4 ),
 ( 0.01291936762762757943, 0.01372441420841338973, 0.01452946078919920003, 0.01533450736998500860, 0.01613955395077081717, 0.01694460053155662921, 0.01774964711234243778, 0.01855469369312824635, 0.01935974027391405838, 0.02016478685469987042, 0.02096983343548567899, 0.02177488001627148756, 0.02257992659705729960, 0.02338497317784310817, 0.02419001975862891674, 0.02459254304902182275, 0.02499506633941472877, 0.02580011292020053734 ),
 .UNSPECIFIED. ) ;
#50464=CARTESIAN_POINT ( 'NONE',  ( -9.333555687487638863, 251.7810269660895699, 3.591168747312683429 ) ) ;
#50514=CARTESIAN_POINT ( 'NONE',  ( 5.475947152006327201, -13.16217730109125306, 2.462898245435121591 ) ) ;
#50517=ORIENTED_EDGE ( 'NONE', *, *, #48161, .T. ) ;
#50522=CARTESIAN_POINT ( 'NONE',  ( -5.855777637195783925, 246.2189350324153736, -1.331220292256674043 ) ) ;
#50553=CARTESIAN_POINT ( 'NONE',  ( -9.220915120640610141, 248.9554511356789988, -3.870126578504832437 ) ) ;
#50557=CARTESIAN_POINT ( 'NONE',  ( 4.521127550501229386, -84.32389759472334845, 3.944701057164354818 ) ) ;
#50574=ADVANCED_FACE ( 'NONE', ( #96716 ), #105333, .F. ) ;
#50690=CARTESIAN_POINT ( 'NONE',  ( -5.650483388624518710, -88.45566596850385110, 2.031129859422142303 ) ) ;
#50721=CARTESIAN_POINT ( 'NONE',  ( -7.801777176595948937, -61.41172014187367267, -1.786991866639924043 ) ) ;
#50935=VERTEX_POINT ( 'NONE', #16309 ) ;
#51089=CARTESIAN_POINT ( 'NONE',  ( -9.999945253488261798, 246.0001368662946390, -0.2662901834230864684 ) ) ;
#51106=AXIS2_PLACEMENT_3D ( 'NONE', #37509, #21316, #71954 ) ;
#51113=ORIENTED_EDGE ( 'NONE', *, *, #17089, .T. ) ;
#51123=CARTESIAN_POINT ( 'NONE',  ( -7.999885325681428405, -6.000229348700641729, 0.2682325777720040438 ) ) ;
#51139=CARTESIAN_POINT ( 'NONE',  ( 6.928203230275507885, -65.00000000000000000, 4.000000000000002665 ) ) ;
#51184=ORIENTED_EDGE ( 'NONE', *, *, #54602, .T. ) ;
#51187=DIRECTION ( 'NONE',  ( 0.000000000000000000, 1.000000000000000000, 0.000000000000000000 ) ) ;
#51318=CARTESIAN_POINT ( 'NONE',  ( 4.472135954999578722, -65.00000000000000000, 4.000000000000002665 ) ) ;
#51346=CARTESIAN_POINT ( 'NONE',  ( -5.646888413699863385, 253.4497415597037389, 2.040714635159906365 ) ) ;
#51349=EDGE_CURVE ( 'NONE', #27454, #20213, #77868, .T. ) ;
#51412=CARTESIAN_POINT ( 'NONE',  ( -5.999787407977319909, -6.000318888155526054, 0.2740427891042984121 ) ) ;
#51539=CARTESIAN_POINT ( 'NONE',  ( 5.855777637195787477, 253.7810649675844559, -1.331220292256661830 ) ) ;
#51577=CARTESIAN_POINT ( 'NONE',  ( -5.477578620271511767, -81.83498560983899495, -2.459398706554656311 ) ) ;
#51661=CARTESIAN_POINT ( 'NONE',  ( -7.801777176595949825, -6.411720141873670009, -1.786991866639922932 ) ) ;
#51801=CARTESIAN_POINT ( 'NONE',  ( 8.000113193197771366, -14.00022638645862827, -0.2613481123984672805 ) ) ;
#51810=ORIENTED_EDGE ( 'NONE', *, *, #7193, .F. ) ;
#51816=VERTEX_POINT ( 'NONE', #54402 ) ;
#51854=EDGE_LOOP ( 'NONE', ( #73260, #9593 ) ) ;
#51876=CARTESIAN_POINT ( 'NONE',  ( -5.981691436642410764, 253.9726909919410787, -0.5384679144502781956 ) ) ;
#51940=CARTESIAN_POINT ( 'NONE',  ( -5.094000037296078531, -7.553658762287765782, -3.174960020027659535 ) ) ;
#52103=CARTESIAN_POINT ( 'NONE',  ( 8.000086790516061086, -60.99982641893993929, 0.2639471549312821241 ) ) ;
#52104=ORIENTED_EDGE ( 'NONE', *, *, #51349, .F. ) ;
#52109=CARTESIAN_POINT ( 'NONE',  ( -4.497472161260645862, -84.45777453374053323, -3.972129482042464410 ) ) ;
#52118=CARTESIAN_POINT ( 'NONE',  ( 5.191472769733073811, -12.64091576718949028, -3.014900733016760537 ) ) ;
#52141=PRESENTATION_STYLE_ASSIGNMENT (( #3613 ) ) ;
#52165=CARTESIAN_POINT ( 'NONE',  ( -9.165151389911699198, 249.7326484439287810, -4.000000000000002665 ) ) ;
#52208=CARTESIAN_POINT ( 'NONE',  ( 7.896254658894416245, -68.78929182754202998, 1.307282859663299712 ) ) ;
#52223=CARTESIAN_POINT ( 'NONE',  ( 5.649205854336966759, 246.5464546718848169, -2.034449005107570763 ) ) ;
#52301=CARTESIAN_POINT ( 'NONE',  ( 5.980543423763064581, -61.02903592498922336, -0.5500789318242889081 ) ) ;
#52351=FILL_AREA_STYLE_COLOUR ( '', #106326 ) ;
#52405=CARTESIAN_POINT ( 'NONE',  ( -5.981118819178464108, 253.9718345618005060, 0.5452870891823475841 ) ) ;
#52627=CARTESIAN_POINT ( 'NONE',  ( 7.986539162393901492, -61.02672828942549899, -0.5321833565149892697 ) ) ;
#52649=CARTESIAN_POINT ( 'NONE',  ( 4.660674839411965920, -11.31782485304406904, -3.778981567323763890 ) ) ;
#52749=EDGE_CURVE ( 'NONE', #73667, #25325, #45014, .T. ) ;
#52756=VERTEX_POINT ( 'NONE', #8949 ) ;
#52872=CARTESIAN_POINT ( 'NONE',  ( 6.928203230275508773, -10.26479267253572480, 3.999999999999999112 ) ) ;
#52902=CARTESIAN_POINT ( 'NONE',  ( 7.801339272325196639, -81.41268528040301078, -1.788609912539668612 ) ) ;
#52926=CARTESIAN_POINT ( 'NONE',  ( -7.801339272325197527, -68.58731471959700343, -1.788609912539672164 ) ) ;
#52967=CIRCLE ( 'NONE', #56399, 10.00000000000003730 ) ;
#52969=EDGE_CURVE ( 'NONE', #92577, #73080, #102874, .T. ) ;
#53019=CARTESIAN_POINT ( 'NONE',  ( -5.856955515201466511, -6.217109411191364288, 1.326217528971455950 ) ) ;
#53073=CARTESIAN_POINT ( 'NONE',  ( 0.000000000000000000, 1.000000000000000888, 0.000000000000000000 ) ) ;
#53207=CARTESIAN_POINT ( 'NONE',  ( -5.383284837158154090, -61.99950656484222122, 2.657356347551696807 ) ) ;
#53304=CARTESIAN_POINT ( 'NONE',  ( 5.999511540169428336, -6.000732691145679532, -0.2833228702578348135 ) ) ;
#53382=CARTESIAN_POINT ( 'NONE',  ( 4.656749229489883568, -63.68239591873568628, -3.785628640239150133 ) ) ;
#53416=CARTESIAN_POINT ( 'NONE',  ( 7.897196874019790869, -13.79127204167806831, -1.302055520192090254 ) ) ;
#53464=CARTESIAN_POINT ( 'NONE',  ( -7.151217271224853178, -66.78749400445718720, -3.587901469523285591 ) ) ;
#53585=CARTESIAN_POINT ( 'NONE',  ( 9.797174393178823685E-16, 0.000000000000000000, 7.999999999999994671 ) ) ;
#53644=CARTESIAN_POINT ( 'NONE',  ( 1.592040838891563829E-15, 1.000000000000000888, 13.00000000000003730 ) ) ;
#53713=AXIS2_PLACEMENT_3D ( 'NONE', #80856, #63644, #73286 ) ;
#53728=ORIENTED_EDGE ( 'NONE', *, *, #15652, .F. ) ;
#53729=CARTESIAN_POINT ( 'NONE',  ( -4.595881407952570719, -63.93374566798679126, -3.857520671226067233 ) ) ;
#53793=CARTESIAN_POINT ( 'NONE',  ( -13.00000000000003730, -65.00000000000000000, 0.000000000000000000 ) ) ;
#53795=ORIENTED_EDGE ( 'NONE', *, *, #79589, .F. ) ;
#53924=CARTESIAN_POINT ( 'NONE',  ( 6.928203230275508773, -10.00000000000001066, -4.000000000000000000 ) ) ;
#53932=VERTEX_POINT ( 'NONE', #26932 ) ;
#53978=CIRCLE ( 'NONE', #29920, 13.00000000000003730 ) ;
#53984=CARTESIAN_POINT ( 'NONE',  ( 7.347880794884120722E-16, -99.99999999999997158, -6.000000000000000888 ) ) ;
#54019=ADVANCED_FACE ( 'NONE', ( #13875 ), #21484, .F. ) ;
#54032=CARTESIAN_POINT ( 'NONE',  ( 4.656390720430120922, -66.31646185960548223, 3.786082374785837867 ) ) ;
#54047=ORIENTED_EDGE ( 'NONE', *, *, #57983, .F. ) ;
#54120=CARTESIAN_POINT ( 'NONE',  ( -6.000469943554648466, -14.00070491670499884, 0.2622423038614475899 ) ) ;
#54144=ORIENTED_EDGE ( 'NONE', *, *, #33390, .T. ) ;
#54176=VERTEX_POINT ( 'NONE', #88325 ) ;
#54228=CARTESIAN_POINT ( 'NONE',  ( -6.943482370013978944, -85.52848370260724664, 3.973876482044368164 ) ) ;
#54233=CARTESIAN_POINT ( 'NONE',  ( -4.589925132946514275, -63.93473983707485786, 3.864926970398267603 ) ) ;
#54272=DIRECTION ( 'NONE',  ( 0.000000000000000000, 0.000000000000000000, -1.000000000000000000 ) ) ;
#54302=PRESENTATION_STYLE_ASSIGNMENT (( #21464 ) ) ;
#54325=CARTESIAN_POINT ( 'NONE',  ( 4.472135954999580498, -10.00000000000000888, 4.000000000000000000 ) ) ;
#54354=CARTESIAN_POINT ( 'NONE',  ( 0.000000000000000000, 4.000000000000003553, -10.00000000000003730 ) ) ;
#54402=CARTESIAN_POINT ( 'NONE',  ( 1.224646799147357595E-15, 4.000000000000003553, 10.00000000000003730 ) ) ;
#54412=EDGE_LOOP ( 'NONE', ( #67969, #92428 ) ) ;
#54435=CARTESIAN_POINT ( 'NONE',  ( -5.477432325710315908, -68.16479535570475434, 2.459915882346688232 ) ) ;
#54556=CARTESIAN_POINT ( 'NONE',  ( -13.00000000000003730, -10.00000000000000888, -4.000000000000000000 ) ) ;
#54583=DIRECTION ( 'NONE',  ( 0.000000000000000000, 0.000000000000000000, -1.000000000000000000 ) ) ;
#54602=EDGE_CURVE ( 'NONE', #104211, #2575, #77119, .T. ) ;
#54645=CARTESIAN_POINT ( 'NONE',  ( 7.212994264445060644, -87.01711344340040455, 3.463766307298588032 ) ) ;
#54652=CARTESIAN_POINT ( 'NONE',  ( -5.192560085536414682, -12.64305442631242826, 3.013051918867554413 ) ) ;
#54710=CARTESIAN_POINT ( 'NONE',  ( 4.472135954999578722, 249.9999999999999432, 4.000000000000002665 ) ) ;
#54947=CARTESIAN_POINT ( 'NONE',  ( 5.728413875956868573, -61.41935773546600785, 1.802282772585246384 ) ) ;
#54957=CYLINDRICAL_SURFACE ( 'NONE', #63291, 4.000000000000002665 ) ;
#54976=CARTESIAN_POINT ( 'NONE',  ( -4.472135954999578722, -65.00000000000000000, 4.000000000000002665 ) ) ;
#55055=CARTESIAN_POINT ( 'NONE',  ( -4.472135954999578722, 249.9999999999999432, -4.000000000000002665 ) ) ;
#55102=CARTESIAN_POINT ( 'NONE',  ( -7.212994264445060644, -62.98288655659961677, 3.463766307298588920 ) ) ;
#55151=CARTESIAN_POINT ( 'NONE',  ( 5.092539576892242792, -87.44323467208434408, 3.177249149099057313 ) ) ;
#55180=EDGE_CURVE ( 'NONE', #15986, #39611, #6532, .T. ) ;
#55190=CARTESIAN_POINT ( 'NONE',  ( -5.728413875956869461, -13.58064226453400281, 1.802282772585246828 ) ) ;
#55253=DIRECTION ( 'NONE',  ( 0.000000000000000000, -0.000000000000000000, 1.000000000000000000 ) ) ;
#55328=CARTESIAN_POINT ( 'NONE',  ( 7.212408192734264034, -7.984829106796318854, -3.465038817813885341 ) ) ;
#55371=ADVANCED_FACE ( 'NONE', ( #91725, #92774 ), #2697, .T. ) ;
#55464=CARTESIAN_POINT ( 'NONE',  ( 4.472135954999579610, -85.00000000000000000, -4.000000000000001776 ) ) ;
#55617=CARTESIAN_POINT ( 'NONE',  ( 5.858824175751780494, -68.78579060872358752, -1.318356988357134441 ) ) ;
#55620=CARTESIAN_POINT ( 'NONE',  ( -7.151597709147948123, -63.21070734947785752, 3.587174531012142342 ) ) ;
#55672=DIRECTION ( 'NONE',  ( -0.000000000000000000, -1.000000000000000000, -0.000000000000000000 ) ) ;
#55876=CARTESIAN_POINT ( 'NONE',  ( -7.801642220026312025, -81.41203173850968255, 1.787233835843583751 ) ) ;
#55916=ORIENTED_EDGE ( 'NONE', *, *, #62948, .T. ) ;
#56018=EDGE_CURVE ( 'NONE', #94625, #19102, #89705, .T. ) ;
#56054=ORIENTED_EDGE ( 'NONE', *, *, #6401, .F. ) ;
#56225=CARTESIAN_POINT ( 'NONE',  ( 7.801777176595948937, -88.58827985812634154, -1.786991866639921822 ) ) ;
#56278=CARTESIAN_POINT ( 'NONE',  ( -7.551437640244098581, -13.00872462522910133, -2.648272645923381408 ) ) ;
#56325=AXIS2_PLACEMENT_3D ( 'NONE', #88924, #98067, #49513 ) ;
#56375=CARTESIAN_POINT ( 'NONE',  ( 9.918325909156591180, 246.2076476829255967, 1.298699613733157232 ) ) ;
#56394=DIRECTION ( 'NONE',  ( 0.000000000000000000, 1.000000000000000000, 0.000000000000000000 ) ) ;
#56399=AXIS2_PLACEMENT_3D ( 'NONE', #35277, #75701, #100506 ) ;
#56462=CARTESIAN_POINT ( 'NONE',  ( 4.472135954999580498, -9.864207950534455094, 4.000000000000000888 ) ) ;
#56482=CIRCLE ( 'NONE', #9985, 7.999999999999994671 ) ;
#56556=PRESENTATION_STYLE_ASSIGNMENT (( #90538 ) ) ;
#56572=CARTESIAN_POINT ( 'NONE',  ( -5.858881034796412202, -68.78586324002981200, 1.317748741875970797 ) ) ;
#56576=FACE_BOUND ( 'NONE', #39984, .T. ) ;
#56671=CARTESIAN_POINT ( 'NONE',  ( -4.905194654929173836, -87.02394395019842932, 3.459476078998853676 ) ) ;
#56692=CARTESIAN_POINT ( 'NONE',  ( -13.00000000000003730, -65.00000000000000000, 0.000000000000000000 ) ) ;
#56696=CARTESIAN_POINT ( 'NONE',  ( -6.944031699373468314, -64.46539345443871127, 3.972913591453824278 ) ) ;
#56796=EDGE_LOOP ( 'NONE', ( #53795, #24894 ) ) ;
#56959=CARTESIAN_POINT ( 'NONE',  ( -9.918512371096326774, 253.7928299227055220, -1.297150762882672614 ) ) ;
#56965=ORIENTED_EDGE ( 'NONE', *, *, #94152, .T. ) ;
#57033=DIRECTION ( 'NONE',  ( 0.000000000000000000, 0.000000000000000000, 1.000000000000000000 ) ) ;
#57076=EDGE_CURVE ( 'NONE', #86829, #45464, #37217, .T. ) ;
#57207=FACE_BOUND ( 'NONE', #8434, .T. ) ;
#57271=CARTESIAN_POINT ( 'NONE',  ( 5.725989721596477899, -88.57677111256464286, 1.809923354557187336 ) ) ;
#57300=CARTESIAN_POINT ( 'NONE',  ( 7.046357527897573192, -86.30615650601002642, -3.789683693877209159 ) ) ;
#57439=CARTESIAN_POINT ( 'NONE',  ( 9.646032546913160033, 246.9871967152563457, 2.644051433538255669 ) ) ;
#57443=CARTESIAN_POINT ( 'NONE',  ( 7.550180524134850302, -6.994407527868143681, 2.651855549982494509 ) ) ;
#57482=CARTESIAN_POINT ( 'NONE',  ( -7.999885325681428405, -81.00022934870062841, 0.2682325777720067084 ) ) ;
#57586=CARTESIAN_POINT ( 'NONE',  ( 6.000469943554648466, -80.99929508329502426, 0.2622423038614462021 ) ) ;
#57603=VERTEX_POINT ( 'NONE', #32295 ) ;
#57628=CARTESIAN_POINT ( 'NONE',  ( 7.619135598915496743, -68.17305367784679504, 2.449260492474797601 ) ) ;
#57729=CARTESIAN_POINT ( 'NONE',  ( -4.472135954999578722, -85.13579204946555024, 4.000000000000001776 ) ) ;
#57754=CARTESIAN_POINT ( 'NONE',  ( -7.046357527897572304, -63.69384349398997358, -3.789683693877210935 ) ) ;
#57924=ORIENTED_EDGE ( 'NONE', *, *, #85905, .F. ) ;
#57983=EDGE_CURVE ( 'NONE', #45464, #86829, #59757, .T. ) ;
#58022=CARTESIAN_POINT ( 'NONE',  ( -7.934203308536662114, -81.13299659982200751, 1.057099537198545214 ) ) ;
#58133=AXIS2_PLACEMENT_3D ( 'NONE', #11512, #28834, #85429 ) ;
#58136=CARTESIAN_POINT ( 'NONE',  ( 5.858881034796412202, -81.21413675997018800, 1.317748741875969687 ) ) ;
#58164=ORIENTED_EDGE ( 'NONE', *, *, #35369, .T. ) ;
#58194=CARTESIAN_POINT ( 'NONE',  ( 4.496882872040831813, 249.4621133451038020, 3.972797206970401174 ) ) ;
#58304=CYLINDRICAL_SURFACE ( 'NONE', #73105, 4.000000000000002665 ) ;
#58343=EDGE_CURVE ( 'NONE', #39277, #63464, #2913, .T. ) ;
#58355=DIRECTION ( 'NONE',  ( -0.000000000000000000, -1.000000000000000000, -0.000000000000000000 ) ) ;
#58356=CARTESIAN_POINT ( 'NONE',  ( 5.981118819178459667, -88.97183456180060546, 0.5452870891823808908 ) ) ;
#58491=VECTOR ( 'NONE', #27313, 1000.000000000000000 ) ;
#58495=ADVANCED_FACE ( 'NONE', ( #96375 ), #18496, .T. ) ;
#58517=ADVANCED_FACE ( 'NONE', ( #23024 ), #14885, .F. ) ;
#58586=CARTESIAN_POINT ( 'NONE',  ( -9.918325909156587628, 253.7923523170740907, 1.298699613733163005 ) ) ;
#58599=CARTESIAN_POINT ( 'NONE',  ( -6.928203230275509661, -10.00000000000000888, 4.000000000000000000 ) ) ;
#58638=CARTESIAN_POINT ( 'NONE',  ( 4.696906829037968301, -11.43998147487893391, -3.734050370377311800 ) ) ;
#58686=CARTESIAN_POINT ( 'NONE',  ( 4.658465013329192494, -83.67636120326905314, 3.783534922165390668 ) ) ;
#58829=CARTESIAN_POINT ( 'NONE',  ( -5.476751506168961114, -88.16357122866993734, -2.461144630687910784 ) ) ;
#58857=CARTESIAN_POINT ( 'NONE',  ( -7.986468734911287726, -61.02686320276919929, 0.5341897780976098131 ) ) ;
#58866=EDGE_LOOP ( 'NONE', ( #29076, #12081 ) ) ;
#58881=CARTESIAN_POINT ( 'NONE',  ( 7.151217271224852290, -83.21250599554284122, -3.587901469523284259 ) ) ;
#58931=CARTESIAN_POINT ( 'NONE',  ( -5.092539576892240127, 252.4432346720841167, 3.177249149099059977 ) ) ;
#58963=CARTESIAN_POINT ( 'NONE',  ( 6.928203230275510549, -10.00000000000000888, 4.000000000000000000 ) ) ;
#59061=( NAMED_UNIT ( * ) PLANE_ANGLE_UNIT ( ) SI_UNIT ( $, .RADIAN. ) );
#59069=AXIS2_PLACEMENT_3D ( 'NONE', #45731, #70547, #27999 ) ;
#59120=CARTESIAN_POINT ( 'NONE',  ( -9.797372177749780420, 253.4650949484755813, 2.014953862275830954 ) ) ;
#59182=CARTESIAN_POINT ( 'NONE',  ( -4.497431761510337189, 249.4590187574896731, -3.972160586670089089 ) ) ;
#59215=CARTESIAN_POINT ( 'NONE',  ( -9.537909130738299268, 247.3538516903660138, -3.010726932293848801 ) ) ;
#59220=CARTESIAN_POINT ( 'NONE',  ( 5.728413875956868573, -81.41935773546600785, 1.802282772585248605 ) ) ;
#59277=CARTESIAN_POINT ( 'NONE',  ( 5.646888413699860720, 246.5502584402960053, 2.040714635159918799 ) ) ;
#59597=SURFACE_STYLE_USAGE ( .BOTH. , #75760 ) ;
#59652=CARTESIAN_POINT ( 'NONE',  ( 5.911778709945828325, 253.8666183941656413, 1.058844270818172451 ) ) ;
#59706=CARTESIAN_POINT ( 'NONE',  ( 5.646888413699863385, -13.44974155970390406, 2.040714635159913914 ) ) ;
#59728=CARTESIAN_POINT ( 'NONE',  ( 7.045755811259133417, -86.30341603013555130, 3.790843699961855773 ) ) ;
#59751=CARTESIAN_POINT ( 'NONE',  ( -9.948513602188008065, 246.1302205665613201, 1.045942665286136775 ) ) ;
#59757=CIRCLE ( 'NONE', #56325, 10.00000000000000178 ) ;
#59783=CARTESIAN_POINT ( 'NONE',  ( -7.046357527897575856, -8.693843493989968252, -3.789683693877206050 ) ) ;
#59798=CARTESIAN_POINT ( 'NONE',  ( 7.413471587080151082, -67.64352159168328171, -3.013058070223549656 ) ) ;
#59811=CARTESIAN_POINT ( 'NONE',  ( 4.660674839411950821, 248.6821751469559274, -3.778981567323782986 ) ) ;
#59932=CARTESIAN_POINT ( 'NONE',  ( 6.928203230275510549, -10.00000000000000888, 4.000000000000000000 ) ) ;
#59933=CARTESIAN_POINT ( 'NONE',  ( -7.619135598915495855, -61.82694632215322628, 2.449260492474798045 ) ) ;
#59956=DIRECTION ( 'NONE',  ( 0.000000000000000000, 0.000000000000000000, 1.000000000000000000 ) ) ;
#60014=CARTESIAN_POINT ( 'NONE',  ( -5.475947152006328977, 253.1621773010911909, 2.462898245435118039 ) ) ;
#60076=CARTESIAN_POINT ( 'NONE',  ( -5.909155701201248334, -6.137383198112712712, 1.073778020691672275 ) ) ;
#60104=ORIENTED_EDGE ( 'NONE', *, *, #31054, .F. ) ;
#60147=PRESENTATION_STYLE_ASSIGNMENT (( #59597 ) ) ;
#60157=CARTESIAN_POINT ( 'NONE',  ( 9.699189539447139907, 246.8230777175328399, -2.444343703917226218 ) ) ;
#60213=EDGE_LOOP ( 'NONE', ( #14699, #36117, #43067, #32899 ) ) ;
#60235=CARTESIAN_POINT ( 'NONE',  ( 7.212408192734266699, -62.98482910679632596, -3.465038817813884009 ) ) ;
#60241=CARTESIAN_POINT ( 'NONE',  ( -5.909155701201243893, -81.13738319811274380, 1.073778020691686486 ) ) ;
#60254=CARTESIAN_POINT ( 'NONE',  ( 4.656390720430125363, -11.31646185960546624, 3.786082374785829430 ) ) ;
#60261=CARTESIAN_POINT ( 'NONE',  ( -5.092539576892241904, -62.55676532791567013, 3.177249149099056869 ) ) ;
#60277=CARTESIAN_POINT ( 'NONE',  ( 7.896254658894418021, -88.78929182754201577, 1.307282859663298158 ) ) ;
#60278=FACE_OUTER_BOUND ( 'NONE', #60213, .T. ) ;
#60325=CARTESIAN_POINT ( 'NONE',  ( -7.801642220026312025, -6.412031738509686107, 1.787233835843581531 ) ) ;
#60352=CARTESIAN_POINT ( 'NONE',  ( 4.589357672516649167, -8.937939690227786116, -3.865585121226769338 ) ) ;
#60426=ORIENTED_EDGE ( 'NONE', *, *, #49055, .F. ) ;
#60466=CARTESIAN_POINT ( 'NONE',  ( 7.896254658894418021, -13.78929182754201044, 1.307282859663291719 ) ) ;
#60513=CARTESIAN_POINT ( 'NONE',  ( -7.550180524134849414, -68.00559247213185188, 2.651855549982493176 ) ) ;
#60537=CARTESIAN_POINT ( 'NONE',  ( -5.383284837158160308, 253.0004934351577504, 2.657356347551687037 ) ) ;
#60606=CARTESIAN_POINT ( 'NONE',  ( 0.000000000000000000, 0.000000000000000000, 0.000000000000000000 ) ) ;
#60618=UNCERTAINTY_MEASURE_WITH_UNIT (LENGTH_MEASURE( 1.000000000000000082E-05 ), #97027, 'distance_accuracy_value', 'NONE');
#60757=CARTESIAN_POINT ( 'NONE',  ( 6.928203230275509661, -65.00000000000000000, -4.000000000000002665 ) ) ;
#60780=CARTESIAN_POINT ( 'NONE',  ( -4.905018583967750700, -62.97640014320320034, -3.459768807258292167 ) ) ;
#60795=CARTESIAN_POINT ( 'NONE',  ( 7.986711519608433285, -88.97361903623433932, -0.5300249774147601789 ) ) ;
#60811=STYLED_ITEM ( 'NONE', ( #60147 ), #101356 ) ;
#60828=ADVANCED_FACE ( 'NONE', ( #16659 ), #74351, .F. ) ;
#60874=CARTESIAN_POINT ( 'NONE',  ( 5.477578620271504661, 246.8349856098389239, -2.459398706554666525 ) ) ;
#60985=CARTESIAN_POINT ( 'NONE',  ( -4.472135954999578722, -65.00000000000000000, -4.000000000000002665 ) ) ;
#61006=DIRECTION ( 'NONE',  ( 0.000000000000000000, 0.000000000000000000, -1.000000000000000000 ) ) ;
#61035=CARTESIAN_POINT ( 'NONE',  ( -6.943482370013977167, -65.52848370260726085, 3.973876482044368164 ) ) ;
#61191=CARTESIAN_POINT ( 'NONE',  ( -4.658465013329193383, -11.32363879673093621, 3.783534922165391112 ) ) ;
#61242=EDGE_CURVE ( 'NONE', #102596, #15986, #56482, .T. ) ;
#61258=ORIENTED_EDGE ( 'NONE', *, *, #48755, .T. ) ;
#61299=CARTESIAN_POINT ( 'NONE',  ( -7.619701877737479201, -88.17442159532768642, -2.447562251315979598 ) ) ;
#61306=CARTESIAN_POINT ( 'NONE',  ( -4.496882872040832702, -64.46211334510377355, 3.972797206970399397 ) ) ;
#61313=AXIS2_PLACEMENT_3D ( 'NONE', #56692, #1089, #34063 ) ;
#61322=CARTESIAN_POINT ( 'NONE',  ( 0.000000000000000000, -100.0000000000000000, 0.000000000000000000 ) ) ;
#61326=CARTESIAN_POINT ( 'NONE',  ( 6.928203230275508773, -85.26479267253573369, 4.000000000000000888 ) ) ;
#61376=CIRCLE ( 'NONE', #13065, 7.999999999999994671 ) ;
#61391=CARTESIAN_POINT ( 'NONE',  ( 6.928203230275509661, -65.00000000000000000, -4.000000000000002665 ) ) ;
#61406=CARTESIAN_POINT ( 'NONE',  ( 5.980543423763066357, -6.029035924989237571, -0.5500789318242828019 ) ) ;
#61409=CARTESIAN_POINT ( 'NONE',  ( 5.191144708981711986, 247.3596991447872142, 3.015512395308856952 ) ) ;
#61491=CARTESIAN_POINT ( 'NONE',  ( 4.472135954999578722, -65.00000000000000000, -4.000000000000002665 ) ) ;
#61493=CARTESIAN_POINT ( 'NONE',  ( 9.999945253488261798, 253.9998631337052757, -0.2662901834231035103 ) ) ;
#61523=CARTESIAN_POINT ( 'NONE',  ( 7.344133061198930612, -12.44494392680577555, 3.176267128233872583 ) ) ;
#61572=EDGE_CURVE ( 'NONE', #49420, #89178, #90226, .T. ) ;
#61573=CARTESIAN_POINT ( 'NONE',  ( -7.150053860865846822, -66.78265453913975591, 3.590189269391292903 ) ) ;
#61671=CARTESIAN_POINT ( 'NONE',  ( -5.725989721596478788, -6.423228887435400658, 1.809923354557177344 ) ) ;
#61674=DIRECTION ( 'NONE',  ( -0.000000000000000000, -1.000000000000000000, -0.000000000000000000 ) ) ;
#61675=EDGE_LOOP ( 'NONE', ( #6245, #51810, #104634, #85453 ) ) ;
#61752=CARTESIAN_POINT ( 'NONE',  ( 0.000000000000000000, 3.999999999999996447, 0.000000000000000000 ) ) ;
#61814=ORIENTED_EDGE ( 'NONE', *, *, #103526, .T. ) ;
#61825=CARTESIAN_POINT ( 'NONE',  ( 7.801339272325197527, -61.41268528040300367, -1.788609912539670166 ) ) ;
#61832=CARTESIAN_POINT ( 'NONE',  ( -5.649205854336970312, -81.54645467188484531, -2.034449005107560549 ) ) ;
#61842=CARTESIAN_POINT ( 'NONE',  ( -7.986452802927061612, -88.97309757691890297, 0.5332468218996310183 ) ) ;
#61848=CARTESIAN_POINT ( 'NONE',  ( -5.981118819178459667, -61.02816543819941586, 0.5452870891823673460 ) ) ;
#62027=CARTESIAN_POINT ( 'NONE',  ( 9.536842176398169002, 252.6423536988397416, 3.014135744008177742 ) ) ;
#62063=CARTESIAN_POINT ( 'NONE',  ( 7.414580834929598296, -12.64656280281483092, 3.010264818013835608 ) ) ;
#62079=CYLINDRICAL_SURFACE ( 'NONE', #100143, 8.000000000000000000 ) ;
#62109=CARTESIAN_POINT ( 'NONE',  ( -6.928203230275505220, -65.26526156932587241, 4.000000000000002665 ) ) ;
#62369=CARTESIAN_POINT ( 'NONE',  ( -7.002641335706725201, -86.05087262680831373, 3.868676264653294172 ) ) ;
#62375=CARTESIAN_POINT ( 'NONE',  ( -4.813668318631093790, -63.20486770173315705, 3.583991016754781267 ) ) ;
#62396=TOROIDAL_SURFACE ( 'NONE', #81296, 12.00000000000003908, 1.000000000000000000 ) ;
#62591=( NAMED_UNIT ( * ) SI_UNIT ( $, .STERADIAN. ) SOLID_ANGLE_UNIT ( ) );
#62596=CARTESIAN_POINT ( 'NONE',  ( 7.211357414135265209, -82.98853460065558352, 3.467230644691329466 ) ) ;
#62716=DIRECTION ( 'NONE',  ( 1.000000000000000000, -0.000000000000000000, -0.000000000000000000 ) ) ;
#62815=FACE_OUTER_BOUND ( 'NONE', #47030, .T. ) ;
#62948=EDGE_CURVE ( 'NONE', #102596, #83184, #39004, .T. ) ;
#63036=CARTESIAN_POINT ( 'NONE',  ( -9.165151389911699198, 249.9999999999999432, 4.000000000000002665 ) ) ;
#63054=EDGE_CURVE ( 'NONE', #1, #104211, #99098, .T. ) ;
#63068=CARTESIAN_POINT ( 'NONE',  ( 5.647817967127100047, -61.54873593471205595, -2.038183545141173614 ) ) ;
#63076=DIRECTION ( 'NONE',  ( 1.000000000000000000, -0.000000000000000000, -0.000000000000000000 ) ) ;
#63166=PRODUCT ( '8. Bar', '8. Bar', '', ( #88649 ) ) ;
#63181=CARTESIAN_POINT ( 'NONE',  ( -4.497472161260654744, 250.5422254662594241, -3.972129482042457749 ) ) ;
#63276=CARTESIAN_POINT ( 'NONE',  ( 4.813668318631095566, -86.79513229826685006, 3.583991016754781711 ) ) ;
#63291=AXIS2_PLACEMENT_3D ( 'NONE', #39344, #63076, #72223 ) ;
#63320=CARTESIAN_POINT ( 'NONE',  ( -5.476751506168963779, -13.16357122866993379, -2.461144630687908119 ) ) ;
#63453=DIRECTION ( 'NONE',  ( 1.000000000000000000, -0.000000000000000000, -0.000000000000000000 ) ) ;
#63464=VERTEX_POINT ( 'NONE', #44721 ) ;
#63506=( NAMED_UNIT ( * ) PLANE_ANGLE_UNIT ( ) SI_UNIT ( $, .RADIAN. ) );
#63644=DIRECTION ( 'NONE',  ( -0.000000000000000000, 1.000000000000000000, -0.000000000000000000 ) ) ;
#63756=CARTESIAN_POINT ( 'NONE',  ( 4.589925132946514275, -66.06526016292515635, 3.864926970398267603 ) ) ;
#63775=B_SPLINE_CURVE_WITH_KNOTS ( 'NONE', 3,
 ( #68402, #10144, #85652, #10665, #18269, #67858, #18819, #43059, #2045, #43580, #69462, #101813, #60325, #34469, #44664, #42511, #51123, #92659, #75946, #3665, #68938, #51661, #27978, #77548, #93733, #92123, #83499, #84584, #36599, #59783, #76467, #11724, #2578, #44123 ),
 .UNSPECIFIED., .F., .F.,
 ( 4, 2, 2, 2, 2, 2, 2, 2, 2, 2, 2, 2, 2, 2, 2, 2, 4 ),
 ( 0.01272238763756221303, 0.01351613129786393037, 0.01430987495816564599, 0.01510361861846736334, 0.01589736227876907895, 0.01669110593907079804, 0.01748484959937251712, 0.01827859325967423273, 0.01907233691997595182, 0.01986608058027767090, 0.02065982424057938999, 0.02145356790088110560, 0.02224731156118282469, 0.02304105522148454377, 0.02383479888178625938, 0.02462854254208798194, 0.02542228620238969755 ),
 .UNSPECIFIED. ) ;
#63832=CARTESIAN_POINT ( 'NONE',  ( -13.00000000000003730, -85.00000000000000000, -4.000000000000001776 ) ) ;
#63936=B_SPLINE_CURVE_WITH_KNOTS ( 'NONE', 3,
 ( #71416, #13180, #7215, #104865, #46107, #88680, #72486, #23442, #104319, #56278, #30468, #89214, #96261, #6151, #32055, #82705, #1221, #8276, #83232, #64933, #49260, #33640, #8809, #49799, #67064, #99944, #106435, #82162, #41716, #74068, #66523, #26117, #65466, #25577 ),
 .UNSPECIFIED., .F., .F.,
 ( 4, 2, 2, 2, 2, 2, 2, 2, 2, 2, 2, 2, 2, 2, 2, 2, 4 ),
 ( 1.734723475976807094E-18, 0.0007951492273476404825, 0.001590298454695279230, 0.002385447682042917978, 0.003180596909390556726, 0.003975746136738195907, 0.004770895364085834221, 0.005566044591433471668, 0.006361193818781109982, 0.007156343046128748296, 0.007951492273476388345, 0.008746641500824024057, 0.009541790728171661504, 0.01033693995551930069, 0.01113208918286693640, 0.01192723841021457558, 0.01272238763756221303 ),
 .UNSPECIFIED. ) ;
#63948=AXIS2_PLACEMENT_3D ( 'NONE', #29362, #104260, #79980 ) ;
#63977=ORIENTED_EDGE ( 'NONE', *, *, #233, .F. ) ;
#63979=( LENGTH_UNIT ( ) NAMED_UNIT ( * ) SI_UNIT ( .MILLI., .METRE. ) );
#64145=CARTESIAN_POINT ( 'NONE',  ( 5.650483388624516046, -61.54433403149616311, 2.031129859422141859 ) ) ;
#64156=FILL_AREA_STYLE_COLOUR ( '', #78444 ) ;
#64176=AXIS2_PLACEMENT_3D ( 'NONE', #23075, #38720, #73169 ) ;
#64248=ORIENTED_EDGE ( 'NONE', *, *, #103526, .F. ) ;
#64264=B_SPLINE_CURVE_WITH_KNOTS ( 'NONE', 3,
 ( #64289, #80972, #56696, #98228, #22253, #55620, #55102, #553, #2178, #91230, #59933, #9736, #100354, #29, #32999, #58857, #73947, #67999, #99273, #90680, #18959, #50721, #35129, #50211, #66394, #92252, #65866, #9208, #25452, #57754, #75551, #66944, #26519, #98746 ),
 .UNSPECIFIED., .F., .F.,
 ( 4, 2, 2, 2, 2, 2, 2, 2, 2, 2, 2, 2, 2, 2, 2, 2, 4 ),
 ( 0.01272238763756221996, 0.01351613129786394946, 0.01430987495816567895, 0.01510361861846740844, 0.01589736227876913793, 0.01669110593907085355, 0.01748484959937256569, 0.01827859325967428131, 0.01907233691997599692, 0.01986608058027770907, 0.02065982424057942468, 0.02145356790088113683, 0.02224731156118284897, 0.02304105522148456459, 0.02383479888178628020, 0.02462854254208799235, 0.02542228620238970449 ),
 .UNSPECIFIED. ) ;
#64289=CARTESIAN_POINT ( 'NONE',  ( -6.928203230275508773, -65.00000000000000000, 4.000000000000002665 ) ) ;
#64369=CARTESIAN_POINT ( 'NONE',  ( 7.551560007654698481, -88.00910351806993503, -2.648022159607833270 ) ) ;
#64387=SHAPE_DEFINITION_REPRESENTATION ( #30457, #84690 ) ;
#64438=DIRECTION ( 'NONE',  ( 0.000000000000000000, 1.000000000000000000, 0.000000000000000000 ) ) ;
#64469=VECTOR ( 'NONE', #35417, 1000.000000000000000 ) ;
#64509=CARTESIAN_POINT ( 'NONE',  ( 9.797372177749775091, 246.5349050515243903, 2.014953862275845609 ) ) ;
#64511=CARTESIAN_POINT ( 'NONE',  ( 7.934914944860276265, -6.131543527998897680, -1.051261972695689328 ) ) ;
#64583=CARTESIAN_POINT ( 'NONE',  ( 5.192560085536412018, -7.356945573687594830, 3.013051918867557077 ) ) ;
#64690=FACE_BOUND ( 'NONE', #14873, .T. ) ;
#64751=AXIS2_PLACEMENT_3D ( 'NONE', #26656, #61674, #43337 ) ;
#64772=EDGE_CURVE ( 'NONE', #45464, #69452, #46080, .T. ) ;
#64796=ORIENTED_EDGE ( 'NONE', *, *, #85983, .T. ) ;
#64850=CARTESIAN_POINT ( 'NONE',  ( 0.000000000000000000, 3.999999999999996447, 0.000000000000000000 ) ) ;
#64880=CARTESIAN_POINT ( 'NONE',  ( 7.003653396366579464, -86.05706205559677358, -3.866846144092870308 ) ) ;
#64933=CARTESIAN_POINT ( 'NONE',  ( -7.934883677559678716, -13.86839177937552314, 1.051380792122691643 ) ) ;
#64952=FACE_OUTER_BOUND ( 'NONE', #19270, .T. ) ;
#65069=CARTESIAN_POINT ( 'NONE',  ( -9.948688207305217190, 253.8702314949018444, -1.044946705213418259 ) ) ;
#65228=VERTEX_POINT ( 'NONE', #104699 ) ;
#65303=ADVANCED_FACE ( 'NONE', ( #23821, #30850 ), #71788, .T. ) ;
#65389=CARTESIAN_POINT ( 'NONE',  ( 5.191144708981714651, -87.64030085521270053, 3.015512395308853844 ) ) ;
#65466=CARTESIAN_POINT ( 'NONE',  ( -6.928203230275510549, -10.26526156932588130, 4.000000000000000888 ) ) ;
#65489=ORIENTED_EDGE ( 'NONE', *, *, #47971, .T. ) ;
#65559=CARTESIAN_POINT ( 'NONE',  ( 7.045965687440313374, -8.696075362139659148, 3.790395326974318024 ) ) ;
#65596=CARTESIAN_POINT ( 'NONE',  ( -7.046357527897573192, -83.69384349398995937, -3.789683693877209159 ) ) ;
#65602=CARTESIAN_POINT ( 'NONE',  ( -9.537927238823533216, 252.6462685711817073, -3.010735687602405619 ) ) ;
#65618=ORIENTED_EDGE ( 'NONE', *, *, #89448, .F. ) ;
#65721=ORIENTED_EDGE ( 'NONE', *, *, #98891, .T. ) ;
#65749=CARTESIAN_POINT ( 'NONE',  ( 7.551892080562057075, -68.00987702539384827, 2.647003822403976248 ) ) ;
#65840=CARTESIAN_POINT ( 'NONE',  ( -4.903871675326606727, -87.02085807301496345, -3.461400506969855684 ) ) ;
#65848=DIRECTION ( 'NONE',  ( 0.000000000000000000, 0.000000000000000000, -1.000000000000000000 ) ) ;
#65866=CARTESIAN_POINT ( 'NONE',  ( -7.344361273354514275, -62.55439469411476239, -3.175733139645589898 ) ) ;
#65907=ORIENTED_EDGE ( 'NONE', *, *, #72594, .T. ) ;
#65916=CARTESIAN_POINT ( 'NONE',  ( 5.727189096784633726, -88.57869875248739788, -1.806430436190347377 ) ) ;
#65946=CYLINDRICAL_SURFACE ( 'NONE', #97245, 4.000000000000001776 ) ;
#66088=ORIENTED_EDGE ( 'NONE', *, *, #63054, .T. ) ;
#66123=CARTESIAN_POINT ( 'NONE',  ( -7.551892080562055298, -81.99012297460615173, 2.647003822403974471 ) ) ;
#66181=EDGE_CURVE ( 'NONE', #53932, #22177, #1059, .T. ) ;
#66287=CARTESIAN_POINT ( 'NONE',  ( 4.472135954999578722, 249.9999999999999432, 4.000000000000002665 ) ) ;
#66367=CARTESIAN_POINT ( 'NONE',  ( -5.382057749264594904, -87.99826798403947237, -2.659775980967107767 ) ) ;
#66394=CARTESIAN_POINT ( 'NONE',  ( -7.551560007654699369, -61.99089648193008628, -2.648022159607837267 ) ) ;
#66417=CARTESIAN_POINT ( 'NONE',  ( 0.000000000000000000, 3.000000000000002665, 12.00000000000003908 ) ) ;
#66522=ORIENTED_EDGE ( 'NONE', *, *, #68044, .T. ) ;
#66523=CARTESIAN_POINT ( 'NONE',  ( -7.002641335706727865, -11.05087262680832971, 3.868676264653292396 ) ) ;
#66593=EDGE_CURVE ( 'NONE', #20213, #27454, #92430, .T. ) ;
#66601=ORIENTED_EDGE ( 'NONE', *, *, #13566, .F. ) ;
#66619=CARTESIAN_POINT ( 'NONE',  ( 6.943482370013978944, -9.471516297392756911, 3.973876482044364611 ) ) ;
#66629=ORIENTED_EDGE ( 'NONE', *, *, #66593, .T. ) ;
#66772=CARTESIAN_POINT ( 'NONE',  ( 5.476751506168961114, -81.83642877133006266, -2.461144630687910784 ) ) ;
#66829=CARTESIAN_POINT ( 'NONE',  ( 4.656390720430122698, 248.6835381403945178, 3.786082374785835203 ) ) ;
#66865=EDGE_CURVE ( 'NONE', #84992, #31964, #47613, .T. ) ;
#66944=CARTESIAN_POINT ( 'NONE',  ( -6.944371705245971249, -64.46100308575449844, -3.972324460300566962 ) ) ;
#67064=CARTESIAN_POINT ( 'NONE',  ( -7.550180524134850302, -13.00559247213187497, 2.651855549982494509 ) ) ;
#67105=CARTESIAN_POINT ( 'NONE',  ( -13.00000000000003730, -10.00000000000000888, 4.000000000000000000 ) ) ;
#67191=VERTEX_POINT ( 'NONE', #91040 ) ;
#67265=CARTESIAN_POINT ( 'NONE',  ( 4.472135954999580498, -10.00000000000000888, 4.000000000000000000 ) ) ;
#67277=CARTESIAN_POINT ( 'NONE',  ( -5.911778709945829213, 246.1333816058341881, 1.058844270818183109 ) ) ;
#67313=CARTESIAN_POINT ( 'NONE',  ( 4.503026011213025370, -84.45658137716684166, 3.965236350746919047 ) ) ;
#67404=CARTESIAN_POINT ( 'NONE',  ( 0.000000000000000000, -99.99999999999997158, 0.000000000000000000 ) ) ;
#67436=ADVANCED_FACE ( 'NONE', ( #70992, #72053 ), #12746, .T. ) ;
#67451=CARTESIAN_POINT ( 'NONE',  ( -5.192560085536412906, -87.64305442631243181, 3.013051918867554413 ) ) ;
#67522=DIRECTION ( 'NONE',  ( -0.000000000000000000, -1.000000000000000000, -0.000000000000000000 ) ) ;
#67524=CARTESIAN_POINT ( 'NONE',  ( 6.928203230275508773, -85.00000000000000000, 4.000000000000001776 ) ) ;
#67653=FACE_BOUND ( 'NONE', #88518, .T. ) ;
#67681=FILL_AREA_STYLE_COLOUR ( '', #76328 ) ;
#67784=CARTESIAN_POINT ( 'NONE',  ( 4.904566723942686224, -12.02242702470747382, 3.460360782932700552 ) ) ;
#67795=CARTESIAN_POINT ( 'NONE',  ( -4.590682673078520182, 248.9320824268784520, 3.864023243754614700 ) ) ;
#67812=DIRECTION ( 'NONE',  ( 0.000000000000000000, 0.000000000000000000, 1.000000000000000000 ) ) ;
#67828=CARTESIAN_POINT ( 'NONE',  ( -9.483056940782047306, 247.5561220989341962, -3.177305548492608711 ) ) ;
#67858=CARTESIAN_POINT ( 'NONE',  ( -7.151597709147949011, -8.210707349477859296, 3.587174531012140122 ) ) ;
#67873=CARTESIAN_POINT ( 'NONE',  ( 7.045755811259132528, -66.30341603013553708, 3.790843699961856217 ) ) ;
#67886=CARTESIAN_POINT ( 'NONE',  ( 5.383284837158151426, 246.9995065648421928, 2.657356347551702580 ) ) ;
#67969=ORIENTED_EDGE ( 'NONE', *, *, #14860, .T. ) ;
#67998=CARTESIAN_POINT ( 'NONE',  ( 7.801642220026312025, -13.58796826149033166, 1.787233835843577534 ) ) ;
#67999=CARTESIAN_POINT ( 'NONE',  ( -8.000113193197771366, -60.99977361354140015, -0.2613481123984653931 ) ) ;
#68044=EDGE_CURVE ( 'NONE', #94625, #67191, #72835, .T. ) ;
#68158=ORIENTED_EDGE ( 'NONE', *, *, #64772, .T. ) ;
#68218=CARTESIAN_POINT ( 'NONE',  ( 9.221346651730858213, 248.9516597993166158, -3.869102247876035072 ) ) ;
#68268=CARTESIAN_POINT ( 'NONE',  ( 5.477432325710311467, 253.1647953557046833, 2.459915882346695337 ) ) ;
#68310=CARTESIAN_POINT ( 'NONE',  ( -5.725989721596477899, -81.42322888743538556, 1.809923354557187336 ) ) ;
#68317=VERTEX_POINT ( 'NONE', #34959 ) ;
#68323=CARTESIAN_POINT ( 'NONE',  ( 4.813668318631101783, -11.79513229826687493, 3.583991016754772829 ) ) ;
#68344=CARTESIAN_POINT ( 'NONE',  ( 7.619135598915496743, -88.17305367784679504, 2.449260492474795825 ) ) ;
#68402=CARTESIAN_POINT ( 'NONE',  ( -6.928203230275509661, -10.00000000000000888, 4.000000000000000000 ) ) ;
#68546=CARTESIAN_POINT ( 'NONE',  ( 7.986468734911285949, -13.97313679723080782, 0.5341897780976077037 ) ) ;
#68630=CARTESIAN_POINT ( 'NONE',  ( -5.649205854336965871, 253.4535453281150410, -2.034449005107577868 ) ) ;
#68813=CARTESIAN_POINT ( 'NONE',  ( 5.980543423763066357, 253.9709640750106985, -0.5500789318242854664 ) ) ;
#68846=CARTESIAN_POINT ( 'NONE',  ( 7.045965687440312486, -63.69607536213965915, 3.790395326974321133 ) ) ;
#68866=CARTESIAN_POINT ( 'NONE',  ( 4.814352310392309597, -11.79678594103575762, -3.583053941560742306 ) ) ;
#68874=CARTESIAN_POINT ( 'NONE',  ( -4.656390720430120922, -63.68353814039456751, 3.786082374785837867 ) ) ;
#68879=CARTESIAN_POINT ( 'NONE',  ( -4.503026011213022706, 249.4565813771667990, 3.965236350746923488 ) ) ;
#68889=CARTESIAN_POINT ( 'NONE',  ( 7.999885325681428405, -88.99977065129938580, 0.2682325777720067084 ) ) ;
#68890=( NAMED_UNIT ( * ) SI_UNIT ( $, .STERADIAN. ) SOLID_ANGLE_UNIT ( ) );
#68910=CARTESIAN_POINT ( 'NONE',  ( -9.253817200599856463, 248.7000727008313277, -3.791916801615155208 ) ) ;
#68938=CARTESIAN_POINT ( 'NONE',  ( -7.897196874019792645, -6.208727958321951235, -1.302055520192089366 ) ) ;
#69045=CARTESIAN_POINT ( 'NONE',  ( 5.982126593009819970, -61.02665772107069131, 0.5333292889181870944 ) ) ;
#69046=CARTESIAN_POINT ( 'NONE',  ( 9.253583916535195186, 251.2980390800503869, 3.792462592445548619 ) ) ;
#69076=CARTESIAN_POINT ( 'NONE',  ( -5.855777637195782148, -68.78106496758447008, -1.331220292256681592 ) ) ;
#69153=CARTESIAN_POINT ( 'NONE',  ( 1.530808498934196254E-15, 0.000000000000000000, 12.00000000000003908 ) ) ;
#69221=CARTESIAN_POINT ( 'NONE',  ( -4.589925132946517827, -8.934739837074847202, 3.864926970398263162 ) ) ;
#69291=CARTESIAN_POINT ( 'NONE',  ( -5.093234209761996034, -12.44467773464909754, 3.176141468578047800 ) ) ;
#69296=CARTESIAN_POINT ( 'NONE',  ( 9.537927238823520781, 247.3537314288182358, -3.010735687602435373 ) ) ;
#69343=DIRECTION ( 'NONE',  ( 1.000000000000000000, -0.000000000000000000, -0.000000000000000000 ) ) ;
#69344=CARTESIAN_POINT ( 'NONE',  ( 5.190609988845230838, 252.6392228674358478, -3.016375611400001322 ) ) ;
#69372=CARTESIAN_POINT ( 'NONE',  ( 7.412906595240166929, -62.35811727147744676, 3.014362223629234894 ) ) ;
#69380=CARTESIAN_POINT ( 'NONE',  ( -5.727189096784633726, -81.42130124751260212, -1.806430436190347377 ) ) ;
#69391=CARTESIAN_POINT ( 'NONE',  ( -7.151217271224852290, -86.78749400445713036, -3.587901469523284259 ) ) ;
#69402=CARTESIAN_POINT ( 'NONE',  ( -4.589357672516645614, 248.9379396902277790, -3.865585121226774667 ) ) ;
#69437=CYLINDRICAL_SURFACE ( 'NONE', #84499, 10.00000000000001954 ) ;
#69452=VERTEX_POINT ( 'NONE', #54354 ) ;
#69462=CARTESIAN_POINT ( 'NONE',  ( -7.619135598915498520, -6.826946322153224500, 2.449260492474796269 ) ) ;
#69476=CARTESIAN_POINT ( 'NONE',  ( 7.986468734911287726, -68.97313679723079360, 0.5341897780976170296 ) ) ;
#69489=CARTESIAN_POINT ( 'NONE',  ( 5.476751506168963779, -6.836428771330083975, -2.461144630687907231 ) ) ;
#69491=CARTESIAN_POINT ( 'NONE',  ( 4.813668318631100007, 248.2048677017330931, 3.583991016754775050 ) ) ;
#69513=EDGE_LOOP ( 'NONE', ( #80863, #79074, #49221, #38067 ) ) ;
#69540=CARTESIAN_POINT ( 'NONE',  ( -13.00000000000003730, 249.9999999999999432, 4.000000000000002665 ) ) ;
#69570=CARTESIAN_POINT ( 'NONE',  ( -13.00000000000003730, -65.00000000000000000, 4.000000000000002665 ) ) ;
#69593=ORIENTED_EDGE ( 'NONE', *, *, #52969, .F. ) ;
#69627=CARTESIAN_POINT ( 'NONE',  ( 7.550180524134850302, -81.99440752786813391, 2.651855549982492732 ) ) ;
#69668=ORIENTED_EDGE ( 'NONE', *, *, #2564, .T. ) ;
#69698=DIRECTION ( 'NONE',  ( 0.000000000000000000, 0.000000000000000000, -1.000000000000000000 ) ) ;
#69739=CARTESIAN_POINT ( 'NONE',  ( -5.191144708981717315, -7.359699144787327008, 3.015512395308848514 ) ) ;
#69781=EDGE_LOOP ( 'NONE', ( #52104, #43136 ) ) ;
#69804=CARTESIAN_POINT ( 'NONE',  ( -5.384233811324312668, -13.00217091344775255, 2.655407383564611923 ) ) ;
#69854=ORIENTED_EDGE ( 'NONE', *, *, #66181, .F. ) ;
#69863=ORIENTED_EDGE ( 'NONE', *, *, #61242, .F. ) ;
#69865=CARTESIAN_POINT ( 'NONE',  ( 4.472135954999579610, 249.9999999999999716, -4.000000000000002665 ) ) ;
#69895=EDGE_CURVE ( 'NONE', #101817, #21035, #85513, .T. ) ;
#69896=CARTESIAN_POINT ( 'NONE',  ( 7.800703710507054467, -61.41404307342057933, 1.791736796405273946 ) ) ;
#69902=CARTESIAN_POINT ( 'NONE',  ( -5.910690929868580135, -81.13504093906810510, -1.065041252563905028 ) ) ;
#69914=CARTESIAN_POINT ( 'NONE',  ( -7.896165657598944065, -88.78911131371972942, -1.307894402814545831 ) ) ;
#69958=CARTESIAN_POINT ( 'NONE',  ( -9.380871178326144033, 247.9888362020166426, 3.467392232194195234 ) ) ;
#70025=ORIENTED_EDGE ( 'NONE', *, *, #66181, .T. ) ;
#70092=CARTESIAN_POINT ( 'NONE',  ( 9.537909130738297492, 252.6461483096339009, -3.010726932293859459 ) ) ;
#70123=CARTESIAN_POINT ( 'NONE',  ( -5.190609988845226397, -67.63922286743593304, -3.016375611400011092 ) ) ;
#70145=FACE_BOUND ( 'NONE', #24445, .T. ) ;
#70149=CARTESIAN_POINT ( 'NONE',  ( 7.150053860865850375, -83.21734546086022988, 3.590189269391291571 ) ) ;
#70175=CARTESIAN_POINT ( 'NONE',  ( -7.414346147791993857, -67.64589157662264540, -3.010818766110536338 ) ) ;
#70206=EDGE_CURVE ( 'NONE', #69452, #51816, #19031, .T. ) ;
#70246=CARTESIAN_POINT ( 'NONE',  ( 4.904566723942681783, -67.02242702470746849, 3.460360782932704549 ) ) ;
#70268=CARTESIAN_POINT ( 'NONE',  ( -4.472135954999581386, -10.00000000000000888, -4.000000000000000000 ) ) ;
#70338=CARTESIAN_POINT ( 'NONE',  ( -4.521127550501230274, -10.67610240527664800, 3.944701057164354818 ) ) ;
#70414=DIRECTION ( 'NONE',  ( 1.000000000000000000, -0.000000000000000000, -0.000000000000000000 ) ) ;
#70437=CARTESIAN_POINT ( 'NONE',  ( -6.000208918519490453, -80.99968662210035575, -0.2646532170642273973 ) ) ;
#70450=CARTESIAN_POINT ( 'NONE',  ( -7.150053860865850375, -86.78265453913975591, 3.590189269391291571 ) ) ;
#70455=CARTESIAN_POINT ( 'NONE',  ( -4.497472161260644086, -64.45777453374053323, -3.972129482042465298 ) ) ;
#70482=CARTESIAN_POINT ( 'NONE',  ( 7.743982712349854580, -6.537869852392644177, 2.020119794285907044 ) ) ;
#70547=DIRECTION ( 'NONE',  ( 1.000000000000000000, -0.000000000000000000, -0.000000000000000000 ) ) ;
#70625=CARTESIAN_POINT ( 'NONE',  ( 4.472135954999577834, -64.72588149001673230, -4.000000000000002665 ) ) ;
#70720=ADVANCED_FACE ( 'NONE', ( #96920 ), #5286, .T. ) ;
#70798=CYLINDRICAL_SURFACE ( 'NONE', #106104, 4.000000000000000000 ) ;
#70992=FACE_BOUND ( 'NONE', #86752, .T. ) ;
#71069=DIRECTION ( 'NONE',  ( 0.000000000000000000, 0.000000000000000000, 1.000000000000000000 ) ) ;
#71234=DIRECTION ( 'NONE',  ( 1.000000000000000000, -0.000000000000000000, -0.000000000000000000 ) ) ;
#71317=CARTESIAN_POINT ( 'NONE',  ( -13.00000000000003730, -10.00000000000000888, 0.000000000000000000 ) ) ;
#71390=ORIENTED_EDGE ( 'NONE', *, *, #40516, .F. ) ;
#71416=CARTESIAN_POINT ( 'NONE',  ( -6.928203230275508773, -10.00000000000000711, -4.000000000000000000 ) ) ;
#71470=DIRECTION ( 'NONE',  ( 0.000000000000000000, 0.000000000000000000, -1.000000000000000000 ) ) ;
#71502=FACE_OUTER_BOUND ( 'NONE', #25970, .T. ) ;
#71519=CARTESIAN_POINT ( 'NONE',  ( 7.151217271224852290, -8.212505995542866088, -3.587901469523287368 ) ) ;
#71565=FILL_AREA_STYLE ('',( #30619 ) ) ;
#71587=CARTESIAN_POINT ( 'NONE',  ( 5.093234209761993370, -7.555322265350923772, 3.176141468578050908 ) ) ;
#71673=FACE_OUTER_BOUND ( 'NONE', #96507, .T. ) ;
#71683=CARTESIAN_POINT ( 'NONE',  ( -9.537291425704626846, 252.6440437733276099, 3.012810007365998022 ) ) ;
#71755=CYLINDRICAL_SURFACE ( 'NONE', #12245, 4.000000000000002665 ) ;
#71788=PLANE ( 'NONE',  #11346 ) ;
#71823=CARTESIAN_POINT ( 'NONE',  ( 4.497472161260645862, -65.54222546625949519, -3.972129482042466186 ) ) ;
#71884=CARTESIAN_POINT ( 'NONE',  ( 9.797174393178825657E-16, -100.0000000000000000, 8.000000000000000000 ) ) ;
#71904=VECTOR ( 'NONE', #78354, 1000.000000000000000 ) ;
#71926=ORIENTED_EDGE ( 'NONE', *, *, #64772, .F. ) ;
#71954=DIRECTION ( 'NONE',  ( 0.000000000000000000, 0.000000000000000000, -1.000000000000000000 ) ) ;
#72020=CARTESIAN_POINT ( 'NONE',  ( 0.000000000000000000, -99.99999999999997158, 6.000000000000000888 ) ) ;
#72053=FACE_OUTER_BOUND ( 'NONE', #51854, .T. ) ;
#72068=CARTESIAN_POINT ( 'NONE',  ( -9.482856158761299170, 247.5569288414526739, 3.177891129109637891 ) ) ;
#72223=DIRECTION ( 'NONE',  ( 0.000000000000000000, 0.000000000000000000, -1.000000000000000000 ) ) ;
#72435=ORIENTED_EDGE ( 'NONE', *, *, #24288, .T. ) ;
#72486=CARTESIAN_POINT ( 'NONE',  ( -7.212408192734265810, -12.01517089320369891, -3.465038817813884897 ) ) ;
#72579=CARTESIAN_POINT ( 'NONE',  ( 9.381394091586589212, 247.9865039441838519, 3.465950112474267542 ) ) ;
#72582=CARTESIAN_POINT ( 'NONE',  ( 7.551437640244098581, -6.991275374770918205, -2.648272645923382296 ) ) ;
#72594=EDGE_CURVE ( 'NONE', #57603, #5539, #89659, .T. ) ;
#72599=( NAMED_UNIT ( * ) PLANE_ANGLE_UNIT ( ) SI_UNIT ( $, .RADIAN. ) );
#72658=CARTESIAN_POINT ( 'NONE',  ( 4.503026011213027147, -9.456581377166838109, 3.965236350746918159 ) ) ;
#72659=FACE_BOUND ( 'NONE', #99608, .T. ) ;
#72688=MECHANICAL_DESIGN_GEOMETRIC_PRESENTATION_REPRESENTATION('',(#36557),#100249);
#72756=CARTESIAN_POINT ( 'NONE',  ( -5.980543423763064581, -68.97096407501076953, -0.5500789318242859105 ) ) ;
#72835=LINE ( 'NONE', #6510, #106428 ) ;
#72841=ORIENTED_EDGE ( 'NONE', *, *, #36291, .T. ) ;
#72897=DIRECTION ( 'NONE',  ( -0.000000000000000000, -1.000000000000000000, -0.000000000000000000 ) ) ;
#72921=CARTESIAN_POINT ( 'NONE',  ( -4.472135954999578722, -65.00000000000000000, -4.000000000000002665 ) ) ;
#73080=VERTEX_POINT ( 'NONE', #104670 ) ;
#73105=AXIS2_PLACEMENT_3D ( 'NONE', #75001, #24900, #49132 ) ;
#73130=CARTESIAN_POINT ( 'NONE',  ( -7.002990960197232440, -83.94733181616541629, 3.868040364119523566 ) ) ;
#73165=LINE ( 'NONE', #106070, #30191 ) ;
#73169=DIRECTION ( 'NONE',  ( 0.000000000000000000, 0.000000000000000000, 1.000000000000000000 ) ) ;
#73260=ORIENTED_EDGE ( 'NONE', *, *, #42885, .T. ) ;
#73286=DIRECTION ( 'NONE',  ( 0.000000000000000000, 0.000000000000000000, 1.000000000000000000 ) ) ;
#73380=CARTESIAN_POINT ( 'NONE',  ( -5.093082057083965886, -87.44446206421569912, -3.176439207277721000 ) ) ;
#73400=FACE_OUTER_BOUND ( 'NONE', #89762, .T. ) ;
#73485=CARTESIAN_POINT ( 'NONE',  ( 6.944371705245973025, -85.53899691424548735, -3.972324460300566962 ) ) ;
#73515=ORIENTED_EDGE ( 'NONE', *, *, #89345, .T. ) ;
#73649=( LENGTH_UNIT ( ) NAMED_UNIT ( * ) SI_UNIT ( .MILLI., .METRE. ) );
#73667=VERTEX_POINT ( 'NONE', #63036 ) ;
#73674=CARTESIAN_POINT ( 'NONE',  ( -7.619135598915496743, -81.82694632215323338, 2.449260492474795825 ) ) ;
#73681=CARTESIAN_POINT ( 'NONE',  ( -9.176803346051528365, 250.5294715579742899, 3.973598758023538124 ) ) ;
#73802=EDGE_CURVE ( 'NONE', #89178, #57603, #46694, .T. ) ;
#73836=AXIS2_PLACEMENT_3D ( 'NONE', #61752, #20795, #95169 ) ;
#73928=CARTESIAN_POINT ( 'NONE',  ( 0.000000000000000000, -100.0000000000000000, 0.000000000000000000 ) ) ;
#73947=CARTESIAN_POINT ( 'NONE',  ( -7.999885325681426629, -61.00022934870061420, 0.2682325777720057647 ) ) ;
#73960=( GEOMETRIC_REPRESENTATION_CONTEXT ( 3 ) GLOBAL_UNCERTAINTY_ASSIGNED_CONTEXT ( ( #4601 ) ) GLOBAL_UNIT_ASSIGNED_CONTEXT ( ( #46399, #103049, #62591 ) ) REPRESENTATION_CONTEXT ( 'NONE', 'WORKASPACE' ) );
#73996=CARTESIAN_POINT ( 'NONE',  ( 4.472135954999577834, -85.27329903512642773, -4.000000000000002665 ) ) ;
#74000=CARTESIAN_POINT ( 'NONE',  ( -6.928203230275506996, -65.26930929695539874, -4.000000000000002665 ) ) ;
#74068=CARTESIAN_POINT ( 'NONE',  ( -7.045965687440315151, -11.30392463786035684, 3.790395326974319801 ) ) ;
#74205=CARTESIAN_POINT ( 'NONE',  ( -6.944031699373470090, -84.46539345443872548, 3.972913591453824278 ) ) ;
#74211=CARTESIAN_POINT ( 'NONE',  ( -9.165151389911699198, 249.9999999999999432, 4.000000000000002665 ) ) ;
#74351=CYLINDRICAL_SURFACE ( 'NONE', #75499, 4.000000000000001776 ) ;
#74486=EDGE_LOOP ( 'NONE', ( #83526, #72435, #25213, #71926 ) ) ;
#74522=DIRECTION ( 'NONE',  ( 0.000000000000000000, 0.000000000000000000, -1.000000000000000000 ) ) ;
#74527=CARTESIAN_POINT ( 'NONE',  ( 6.000208918519490453, -89.00031337789968688, -0.2646532170642273973 ) ) ;
#74642=DIRECTION ( 'NONE',  ( 1.000000000000000000, -0.000000000000000000, -0.000000000000000000 ) ) ;
#74690=CARTESIAN_POINT ( 'NONE',  ( 9.482945380845317018, 247.5566694122106242, 3.177595346755247796 ) ) ;
#74727=AXIS2_PLACEMENT_3D ( 'NONE', #88052, #72897, #48092 ) ;
#74733=CARTESIAN_POINT ( 'NONE',  ( -6.928203230275508773, -84.73520732746429474, 4.000000000000000888 ) ) ;
#74819=APPLICATION_CONTEXT ( 'automotive_design' ) ;
#74891=CARTESIAN_POINT ( 'NONE',  ( 4.472135954999577834, 249.7292277993263383, 4.000000000000005329 ) ) ;
#74994=CYLINDRICAL_SURFACE ( 'NONE', #61313, 4.000000000000002665 ) ;
#75001=CARTESIAN_POINT ( 'NONE',  ( -13.00000000000003730, 249.9999999999999432, 0.000000000000000000 ) ) ;
#75027=CARTESIAN_POINT ( 'NONE',  ( 7.002619243997878939, -83.94992681986181537, -3.868708944012999584 ) ) ;
#75050=CARTESIAN_POINT ( 'NONE',  ( 5.858824175751784047, -88.78579060872363016, -1.318356988357131998 ) ) ;
#75338=CARTESIAN_POINT ( 'NONE',  ( -5.647817967127105376, 246.5487359347119991, -2.038183545141165176 ) ) ;
#75374=CARTESIAN_POINT ( 'NONE',  ( -9.645512969475880993, 246.9889684932426803, -2.645801731561377768 ) ) ;
#75380=CARTESIAN_POINT ( 'NONE',  ( 4.589357672516646502, -83.93793969022777901, -3.865585121226772891 ) ) ;
#75423=CARTESIAN_POINT ( 'NONE',  ( -13.00000000000003730, -85.00000000000000000, 0.000000000000000000 ) ) ;
#75499=AXIS2_PLACEMENT_3D ( 'NONE', #75423, #429, #25314 ) ;
#75522=CARTESIAN_POINT ( 'NONE',  ( -5.909259836070535954, -88.86277204242071548, -1.072443315311454981 ) ) ;
#75551=CARTESIAN_POINT ( 'NONE',  ( -7.003653396366579464, -63.94293794440324064, -3.866846144092871196 ) ) ;
#75657=TOROIDAL_SURFACE ( 'NONE', #96336, 12.00000000000003908, 1.000000000000000000 ) ;
#75701=DIRECTION ( 'NONE',  ( -0.000000000000000000, -1.000000000000000000, -0.000000000000000000 ) ) ;
#75760=SURFACE_SIDE_STYLE ('',( #43406 ) ) ;
#75847=ORIENTED_EDGE ( 'NONE', *, *, #18727, .T. ) ;
#75919=CARTESIAN_POINT ( 'NONE',  ( 4.813555570991609578, -83.20526203482680216, -3.584128953194789968 ) ) ;
#75946=CARTESIAN_POINT ( 'NONE',  ( -7.986711519608433285, -6.026380963765670451, -0.5300249774147614001 ) ) ;
#76131=CARTESIAN_POINT ( 'NONE',  ( -7.045965687440310710, -66.30392463786034796, 3.790395326974320689 ) ) ;
#76259=CARTESIAN_POINT ( 'NONE',  ( 7.347880794884120722E-16, -99.99999999999997158, -6.000000000000000888 ) ) ;
#76288=( NAMED_UNIT ( * ) SI_UNIT ( $, .STERADIAN. ) SOLID_ANGLE_UNIT ( ) );
#76328=COLOUR_RGB ( '', 0.09019608, 0.27058824, 0.51372549) ;
#76340=CARTESIAN_POINT ( 'NONE',  ( 5.728413875956875678, 253.5806422645339637, 1.802282772585232173 ) ) ;
#76356=CARTESIAN_POINT ( 'NONE',  ( -13.00000000000003730, -65.00000000000000000, -4.000000000000002665 ) ) ;
#76391=CARTESIAN_POINT ( 'NONE',  ( 5.909155701201247446, -13.86261680188730772, 1.073778020691672941 ) ) ;
#76400=CARTESIAN_POINT ( 'NONE',  ( -5.728413875956867685, 246.4193577354659510, 1.802282772585255266 ) ) ;
#76413=CARTESIAN_POINT ( 'NONE',  ( 7.551892080562055298, -88.00987702539381985, 2.647003822403974471 ) ) ;
#76434=CARTESIAN_POINT ( 'NONE',  ( -9.918010731619586906, 246.2084831515677195, -1.300854425901577516 ) ) ;
#76467=CARTESIAN_POINT ( 'NONE',  ( -7.003653396366583905, -8.942937944403233530, -3.866846144092864535 ) ) ;
#76484=CARTESIAN_POINT ( 'NONE',  ( 7.551560007654697593, -68.00910351806993503, -2.648022159607834602 ) ) ;
#76498=CARTESIAN_POINT ( 'NONE',  ( 4.903871675326607615, -7.979141926985056976, -3.461400506969853463 ) ) ;
#76500=CARTESIAN_POINT ( 'NONE',  ( 5.981691436642411652, 246.0273090080588361, -0.5384679144502751980 ) ) ;
#76531=DIRECTION ( 'NONE',  ( 1.000000000000000000, -0.000000000000000000, -0.000000000000000000 ) ) ;
#76574=CARTESIAN_POINT ( 'NONE',  ( 9.798380800342677333, 253.4680065431550986, -2.010350564680340568 ) ) ;
#76607=CARTESIAN_POINT ( 'NONE',  ( 7.413471587080152858, -12.64352159168328171, -3.013058070223546991 ) ) ;
#76659=CARTESIAN_POINT ( 'NONE',  ( -7.743982712349853692, -68.46213014760736826, 2.020119794285911041 ) ) ;
#76876=CARTESIAN_POINT ( 'NONE',  ( 4.905194654929182718, 252.0239439501984009, 3.459476078998841242 ) ) ;
#76914=CARTESIAN_POINT ( 'NONE',  ( 7.550180524134850302, -61.99440752786815523, 2.651855549982495397 ) ) ;
#76918=VERTEX_POINT ( 'NONE', #53984 ) ;
#76922=CARTESIAN_POINT ( 'NONE',  ( -5.092539576892242792, -82.55676532791565592, 3.177249149099057313 ) ) ;
#76930=CYLINDRICAL_SURFACE ( 'NONE', #88769, 4.000000000000002665 ) ;
#76939=CARTESIAN_POINT ( 'NONE',  ( -5.191144708981716427, -62.35969914478732079, 3.015512395308852067 ) ) ;
#76944=CARTESIAN_POINT ( 'NONE',  ( -4.472135954999578722, 249.9999999999999432, -4.000000000000002665 ) ) ;
#76953=CARTESIAN_POINT ( 'NONE',  ( 6.928203230275508773, -85.00000000000000000, 4.000000000000001776 ) ) ;
#76975=CARTESIAN_POINT ( 'NONE',  ( -9.798380800342682662, 246.5319934568448730, -2.010350564680316143 ) ) ;
#77038=CARTESIAN_POINT ( 'NONE',  ( 4.813555570991616683, -8.205262034826786177, -3.584128953194781975 ) ) ;
#77119=LINE ( 'NONE', #69570, #95323 ) ;
#77120=CARTESIAN_POINT ( 'NONE',  ( 5.999511540169427448, -61.00073269114566443, -0.2833228702578399760 ) ) ;
#77153=CARTESIAN_POINT ( 'NONE',  ( -4.903871675326605839, -67.02085807301496345, -3.461400506969857016 ) ) ;
#77178=CARTESIAN_POINT ( 'NONE',  ( 7.986452802927061612, -81.02690242308115387, 0.5332468218996310183 ) ) ;
#77181=EDGE_CURVE ( 'NONE', #73080, #54176, #36678, .T. ) ;
#77204=CARTESIAN_POINT ( 'NONE',  ( -7.999912353029502654, -68.99982470603094953, -0.2691822806795026723 ) ) ;
#77232=ORIENTED_EDGE ( 'NONE', *, *, #102723, .T. ) ;
#77297=CARTESIAN_POINT ( 'NONE',  ( -4.496882872040837142, -9.462113345103771778, 3.972797206970396733 ) ) ;
#77311=AXIS2_PLACEMENT_3D ( 'NONE', #73928, #32978, #65848 ) ;
#77354=DIRECTION ( 'NONE',  ( 0.000000000000000000, 1.000000000000000000, 0.000000000000000000 ) ) ;
#77464=CARTESIAN_POINT ( 'NONE',  ( -5.383284837158154978, -81.99950656484222122, 2.657356347551699027 ) ) ;
#77475=CARTESIAN_POINT ( 'NONE',  ( 4.595881407952573383, -11.06625433201323894, -3.857520671226066344 ) ) ;
#77477=CARTESIAN_POINT ( 'NONE',  ( -7.002619243997878939, -86.05007318013817041, -3.868708944012999584 ) ) ;
#77548=CARTESIAN_POINT ( 'NONE',  ( -7.619753052866897747, -6.825484971928266198, -2.447276542590447246 ) ) ;
#77564=CARTESIAN_POINT ( 'NONE',  ( 6.928203230275506108, -65.26883324508997930, -4.000000000000002665 ) ) ;
#77661=CARTESIAN_POINT ( 'NONE',  ( 9.989435848181802413, 253.9738029252842182, -0.5278651953176168865 ) ) ;
#77692=CARTESIAN_POINT ( 'NONE',  ( -5.476751506168961114, -68.16357122866992313, -2.461144630687911228 ) ) ;
#77708=SURFACE_STYLE_FILL_AREA ( #103566 ) ;
#77729=AXIS2_PLACEMENT_3D ( 'NONE', #23126, #48422, #89438 ) ;
#77868=CIRCLE ( 'NONE', #3794, 6.000000000000000888 ) ;
#78000=CARTESIAN_POINT ( 'NONE',  ( 4.472135954999581386, -10.27329903512641884, -4.000000000000000000 ) ) ;
#78002=CARTESIAN_POINT ( 'NONE',  ( -7.934883677559678716, -88.86839177937552847, 1.051380792122687202 ) ) ;
#78007=CARTESIAN_POINT ( 'NONE',  ( -5.649205854336968535, -61.54645467188483821, -2.034449005107563657 ) ) ;
#78062=ORIENTED_EDGE ( 'NONE', *, *, #85200, .T. ) ;
#78085=CARTESIAN_POINT ( 'NONE',  ( 7.046357527897571416, -66.30615650601004063, -3.789683693877209603 ) ) ;
#78099=CARTESIAN_POINT ( 'NONE',  ( 5.911778709945828325, -6.133381605834290262, 1.058844270818177336 ) ) ;
#78212=CARTESIAN_POINT ( 'NONE',  ( 6.928203230275510549, -10.26883324508999173, -4.000000000000000888 ) ) ;
#78233=CARTESIAN_POINT ( 'NONE',  ( 7.896165657598944065, -81.21088868628027058, -1.307894402814545831 ) ) ;
#78259=CARTESIAN_POINT ( 'NONE',  ( -7.800703710507054467, -68.58595692657939935, 1.791736796405269283 ) ) ;
#78299=ORIENTED_EDGE ( 'NONE', *, *, #82355, .T. ) ;
#78319=DIRECTION ( 'NONE',  ( 1.000000000000000000, -0.000000000000000000, -0.000000000000000000 ) ) ;
#78344=CARTESIAN_POINT ( 'NONE',  ( -5.382954851612916869, -7.000125085105551648, -2.657971597726727975 ) ) ;
#78354=DIRECTION ( 'NONE',  ( 1.000000000000000000, -0.000000000000000000, -0.000000000000000000 ) ) ;
#78415=CARTESIAN_POINT ( 'NONE',  ( -5.858881034796412202, -13.78586324002981733, 1.317748741875968355 ) ) ;
#78444=COLOUR_RGB ( '', 0.09019608, 0.27058824, 0.51372549) ;
#78508=CARTESIAN_POINT ( 'NONE',  ( -4.496882872040834478, -84.46211334510377355, 3.972797206970398509 ) ) ;
#78520=CARTESIAN_POINT ( 'NONE',  ( -7.211357414135265209, -87.01146539934438806, 3.467230644691329466 ) ) ;
#78538=CIRCLE ( 'NONE', #32053, 6.000000000000000888 ) ;
#78556=CARTESIAN_POINT ( 'NONE',  ( 7.934883677559682269, -6.131608220624498173, 1.051380792122689423 ) ) ;
#78725=CARTESIAN_POINT ( 'NONE',  ( 7.619753052866895970, -13.17451502807175068, -2.447276542590446802 ) ) ;
#78751=CARTESIAN_POINT ( 'NONE',  ( 6.943482370013978944, -84.47151629739272494, 3.973876482044368164 ) ) ;
#78754=CARTESIAN_POINT ( 'NONE',  ( 4.472135954999580498, -10.00000000000000888, 4.000000000000000000 ) ) ;
#78831=ADVANCED_FACE ( 'NONE', ( #80808, #9568 ), #69437, .T. ) ;
#78833=ORIENTED_EDGE ( 'NONE', *, *, #48161, .F. ) ;
#78854=CARTESIAN_POINT ( 'NONE',  ( 5.646888413699862497, -68.44974155970390939, 2.040714635159915247 ) ) ;
#78931=EDGE_CURVE ( 'NONE', #25325, #73667, #14844, .T. ) ;
#78936=VERTEX_POINT ( 'NONE', #47252 ) ;
#78948=CARTESIAN_POINT ( 'NONE',  ( -5.911778709945830101, -13.86661839416573194, 1.058844270818175115 ) ) ;
#79062=CARTESIAN_POINT ( 'NONE',  ( -6.928203230275509661, -85.26526156932588663, 4.000000000000001776 ) ) ;
#79074=ORIENTED_EDGE ( 'NONE', *, *, #61242, .T. ) ;
#79091=CARTESIAN_POINT ( 'NONE',  ( 7.986539162393901492, -6.026728289425493656, -0.5321833565149887146 ) ) ;
#79128=DIRECTION ( 'NONE',  ( 0.000000000000000000, 0.000000000000000000, -1.000000000000000000 ) ) ;
#79291=CARTESIAN_POINT ( 'NONE',  ( 7.618844049274129837, -81.82764101070539198, 2.450177051822847840 ) ) ;
#79337=COLOUR_RGB ( '', 0.09019608, 0.27058824, 0.51372549) ;
#79389=CARTESIAN_POINT ( 'NONE',  ( 5.725989721596477011, -68.57677111256458602, 1.809923354557184894 ) ) ;
#79441=CARTESIAN_POINT ( 'NONE',  ( 4.496882872040834478, -85.53788665489625487, 3.972797206970398509 ) ) ;
#79481=CARTESIAN_POINT ( 'NONE',  ( -4.472135954999581386, -10.13579204946556089, 4.000000000000001776 ) ) ;
#79534=CARTESIAN_POINT ( 'NONE',  ( 4.521127550501233827, 250.6761024052766516, 3.944701057164349933 ) ) ;
#79589=EDGE_CURVE ( 'NONE', #4111, #54176, #90898, .T. ) ;
#79668=DIRECTION ( 'NONE',  ( 0.000000000000000000, 0.000000000000000000, -1.000000000000000000 ) ) ;
#79688=CARTESIAN_POINT ( 'NONE',  ( 5.650483388624516046, -6.544334031496181758, 2.031129859422145856 ) ) ;
#79689=FACE_BOUND ( 'NONE', #54412, .T. ) ;
#79800=CARTESIAN_POINT ( 'NONE',  ( -4.478476647430157165, -65.27352079182048783, 3.992942460563209117 ) ) ;
#79980=DIRECTION ( 'NONE',  ( 0.000000000000000000, 0.000000000000000000, -1.000000000000000000 ) ) ;
#80056=CARTESIAN_POINT ( 'NONE',  ( 4.503026011213026258, 250.5434186228332010, 3.965236350746919047 ) ) ;
#80146=LINE ( 'NONE', #50423, #28194 ) ;
#80157=FILL_AREA_STYLE ('',( #40761 ) ) ;
#80322=ORIENTED_EDGE ( 'NONE', *, *, #40628, .F. ) ;
#80440=CARTESIAN_POINT ( 'NONE',  ( 4.567209634097048720, -65.93599786085512449, -3.891254717191803714 ) ) ;
#80620=DIRECTION ( 'NONE',  ( -0.000000000000000000, -1.000000000000000000, -0.000000000000000000 ) ) ;
#80702=CARTESIAN_POINT ( 'NONE',  ( -7.896254658894418021, -81.21070817245801265, 1.307282859663298158 ) ) ;
#80808=FACE_BOUND ( 'NONE', #56796, .T. ) ;
#80822=CARTESIAN_POINT ( 'NONE',  ( 4.478476647430158941, -64.72647920817954059, 3.992942460563209117 ) ) ;
#80852=CARTESIAN_POINT ( 'NONE',  ( -4.503026011213025370, -65.54341862283317255, 3.965236350746919047 ) ) ;
#80856=CARTESIAN_POINT ( 'NONE',  ( 0.000000000000000000, -99.99999999999997158, 0.000000000000000000 ) ) ;
#80863=ORIENTED_EDGE ( 'NONE', *, *, #62948, .F. ) ;
#80972=CARTESIAN_POINT ( 'NONE',  ( -6.928203230275507885, -64.73520732746426631, 4.000000000000002665 ) ) ;
#81050=CARTESIAN_POINT ( 'NONE',  ( 7.150931910075641440, -86.78625798522261903, -3.588457848165358843 ) ) ;
#81206=PRESENTATION_STYLE_ASSIGNMENT (( #98461 ) ) ;
#81269=CARTESIAN_POINT ( 'NONE',  ( 0.000000000000000000, 1.000000000000000888, -12.00000000000003908 ) ) ;
#81296=AXIS2_PLACEMENT_3D ( 'NONE', #85603, #23934, #40604 ) ;
#81358=( NAMED_UNIT ( * ) SI_UNIT ( $, .STERADIAN. ) SOLID_ANGLE_UNIT ( ) );
#81464=CARTESIAN_POINT ( 'NONE',  ( 9.165151389911699198, 249.9999999999999432, -4.000000000000002665 ) ) ;
#81516=ADVANCED_FACE ( 'NONE', ( #97102 ), #71755, .F. ) ;
#81533=CARTESIAN_POINT ( 'NONE',  ( 5.477578620271511767, -88.16501439016107611, -2.459398706554656311 ) ) ;
#81752=CARTESIAN_POINT ( 'NONE',  ( -7.897196874019792645, -81.20872795832192992, -1.302055520192090032 ) ) ;
#81861=CARTESIAN_POINT ( 'NONE',  ( 5.911778709945830101, -81.13338160583427339, 1.058844270818174227 ) ) ;
#81909=CARTESIAN_POINT ( 'NONE',  ( 7.344133061198927059, -67.44494392680579153, 3.176267128233876136 ) ) ;
#82005=CARTESIAN_POINT ( 'NONE',  ( -4.472135954999579610, -85.00000000000000000, 4.000000000000001776 ) ) ;
#82008=DIRECTION ( 'NONE',  ( -0.000000000000000000, -1.000000000000000000, -0.000000000000000000 ) ) ;
#82083=DIRECTION ( 'NONE',  ( 0.000000000000000000, 1.000000000000000000, 0.000000000000000000 ) ) ;
#82085=CARTESIAN_POINT ( 'NONE',  ( 4.660674839411966808, -86.31782485304408681, -3.778981567323765223 ) ) ;
#82091=CARTESIAN_POINT ( 'NONE',  ( -6.928203230275509661, -65.00000000000000000, -4.000000000000002665 ) ) ;
#82162=CARTESIAN_POINT ( 'NONE',  ( -7.211357414135266097, -12.01146539934442359, 3.467230644691328578 ) ) ;
#82304=CARTESIAN_POINT ( 'NONE',  ( -7.150931910075641440, -83.21374201477736676, -3.588457848165358843 ) ) ;
#82355=EDGE_CURVE ( 'NONE', #68317, #36313, #19315, .T. ) ;
#82390=ADVANCED_FACE ( 'NONE', ( #60278 ), #62396, .T. ) ;
#82557=CARTESIAN_POINT ( 'NONE',  ( -6.000469943554648466, -89.00070491670501838, 0.2622423038614462021 ) ) ;
#82595=VECTOR ( 'NONE', #94599, 1000.000000000000000 ) ;
#82705=CARTESIAN_POINT ( 'NONE',  ( -7.986539162393899716, -13.97327171057452411, -0.5321833565149880485 ) ) ;
#82726=AXIS2_PLACEMENT_3D ( 'NONE', #88825, #31155, #79668 ) ;
#82841=CARTESIAN_POINT ( 'NONE',  ( -6.928203230275508773, -84.73116675491002070, -4.000000000000002665 ) ) ;
#82905=ORIENTED_EDGE ( 'NONE', *, *, #29209, .F. ) ;
#82951=CARTESIAN_POINT ( 'NONE',  ( 4.472135954999578722, -84.86420795053444976, 4.000000000000001776 ) ) ;
#83088=CARTESIAN_POINT ( 'NONE',  ( -4.589357672516646502, -86.06206030977220678, -3.865585121226772891 ) ) ;
#83154=DIRECTION ( 'NONE',  ( -0.000000000000000000, -1.000000000000000000, -0.000000000000000000 ) ) ;
#83158=DIRECTION ( 'NONE',  ( 0.000000000000000000, 1.000000000000000000, 0.000000000000000000 ) ) ;
#83184=VERTEX_POINT ( 'NONE', #31235 ) ;
#83188=CARTESIAN_POINT ( 'NONE',  ( -4.696906829037965636, 251.4399814748788913, -3.734050370377318018 ) ) ;
#83232=CARTESIAN_POINT ( 'NONE',  ( -7.986452802927061612, -13.97309757691886922, 0.5332468218996361253 ) ) ;
#83374=CARTESIAN_POINT ( 'NONE',  ( -9.646083234704192932, 253.0129060902346794, -2.643797197754266026 ) ) ;
#83425=FACE_OUTER_BOUND ( 'NONE', #105578, .T. ) ;
#83475=CARTESIAN_POINT ( 'NONE',  ( 5.647817967127097383, -81.54873593471207016, -2.038183545141173614 ) ) ;
#83499=CARTESIAN_POINT ( 'NONE',  ( -7.344361273354514275, -7.554394694114762387, -3.175733139645582792 ) ) ;
#83526=ORIENTED_EDGE ( 'NONE', *, *, #57983, .T. ) ;
#83545=EDGE_LOOP ( 'NONE', ( #64796, #61814 ) ) ;
#83562=LINE ( 'NONE', #10205, #91012 ) ;
#83607=CARTESIAN_POINT ( 'NONE',  ( -5.477432325710316796, -88.16479535570472592, 2.459915882346686899 ) ) ;
#83710=CARTESIAN_POINT ( 'NONE',  ( -5.191144708981720868, 252.6403008552126721, 3.015512395308842297 ) ) ;
#84014=CARTESIAN_POINT ( 'NONE',  ( 5.093234209761996922, -82.55532226535090956, 3.176141468578046023 ) ) ;
#84148=CARTESIAN_POINT ( 'NONE',  ( -6.928203230275508773, -65.00000000000000000, 4.000000000000002665 ) ) ;
#84330=DIRECTION ( 'NONE',  ( 0.000000000000000000, 0.000000000000000000, -1.000000000000000000 ) ) ;
#84453=CARTESIAN_POINT ( 'NONE',  ( 5.093082057083956116, 252.4444620642155996, -3.176439207277734766 ) ) ;
#84485=CARTESIAN_POINT ( 'NONE',  ( 7.618844049274132502, -61.82764101070539908, 2.450177051822849617 ) ) ;
#84493=CARTESIAN_POINT ( 'NONE',  ( -4.696906829037973630, -83.56001852512108030, -3.734050370377307360 ) ) ;
#84499=AXIS2_PLACEMENT_3D ( 'NONE', #101785, #44090, #27953 ) ;
#84550=CARTESIAN_POINT ( 'NONE',  ( -9.842473135306432752, 246.4106818288640568, 1.785129593756279220 ) ) ;
#84584=CARTESIAN_POINT ( 'NONE',  ( -7.213352437320215138, -7.981635269923192055, -3.463014597543478512 ) ) ;
#84690=SHAPE_REPRESENTATION ( '8. Bar', ( #10728 ), #90114 ) ;
#84691=DIRECTION ( 'NONE',  ( 0.000000000000000000, 0.000000000000000000, -1.000000000000000000 ) ) ;
#84794=CARTESIAN_POINT ( 'NONE',  ( -6.000208918519490453, 254.0003133778996300, -0.2646532170642417747 ) ) ;
#84846=EDGE_LOOP ( 'NONE', ( #21919, #7860, #28126, #13914 ) ) ;
#84854=CARTESIAN_POINT ( 'NONE',  ( -4.905018583967756030, -7.976400143203195903, -3.459768807258288170 ) ) ;
#84855=EDGE_LOOP ( 'NONE', ( #84938, #104633, #71390, #90524 ) ) ;
#84933=CARTESIAN_POINT ( 'NONE',  ( 9.381593208289393360, 247.9856136188048765, -3.465401811657803144 ) ) ;
#84938=ORIENTED_EDGE ( 'NONE', *, *, #88910, .T. ) ;
#84992=VERTEX_POINT ( 'NONE', #22525 ) ;
#85012=CARTESIAN_POINT ( 'NONE',  ( 7.934883677559680493, -61.13160822062448574, 1.051380792122691421 ) ) ;
#85021=CARTESIAN_POINT ( 'NONE',  ( -4.472135954999577834, -84.72670096487358649, -4.000000000000002665 ) ) ;
#85035=CARTESIAN_POINT ( 'NONE',  ( -7.986539162393897939, -88.97327171057455075, -0.5321833565149911571 ) ) ;
#85077=CARTESIAN_POINT ( 'NONE',  ( -9.948561005166148163, 246.1300972625179782, -1.045755304005127062 ) ) ;
#85132=CARTESIAN_POINT ( 'NONE',  ( 5.382057749264598456, -7.001732015960572042, -2.659775980967105991 ) ) ;
#85134=CARTESIAN_POINT ( 'NONE',  ( 5.999787407977320797, 246.0003188881554763, 0.2740427891042969688 ) ) ;
#85200=EDGE_CURVE ( 'NONE', #1, #12726, #12686, .T. ) ;
#85210=CARTESIAN_POINT ( 'NONE',  ( 5.190609988845225509, -62.36077713256408828, -3.016375611400011092 ) ) ;
#85263=SURFACE_SIDE_STYLE ('',( #77708 ) ) ;
#85269=CARTESIAN_POINT ( 'NONE',  ( 7.896571385775229324, -81.21002000654247865, 1.305932416347435732 ) ) ;
#85272=CARTESIAN_POINT ( 'NONE',  ( -6.928203230275507885, -85.00000000000000000, -4.000000000000001776 ) ) ;
#85274=PRODUCT_DEFINITION_FORMATION_WITH_SPECIFIED_SOURCE ( 'ANY', '', #63166, .NOT_KNOWN. ) ;
#85325=CARTESIAN_POINT ( 'NONE',  ( -5.910690929868577470, 253.8649590609318807, -1.065041252563913465 ) ) ;
#85328=EDGE_LOOP ( 'NONE', ( #98988, #40154, #46101, #94926 ) ) ;
#85429=DIRECTION ( 'NONE',  ( 0.000000000000000000, 0.000000000000000000, -1.000000000000000000 ) ) ;
#85430=ORIENTED_EDGE ( 'NONE', *, *, #21730, .T. ) ;
#85453=ORIENTED_EDGE ( 'NONE', *, *, #32427, .T. ) ;
#85513=LINE ( 'NONE', #44521, #58491 ) ;
#85524=CARTESIAN_POINT ( 'NONE',  ( 4.815811321232740916, 251.8007670769736990, 3.581116321197037156 ) ) ;
#85560=CARTESIAN_POINT ( 'NONE',  ( 7.002641335706726977, -63.94912737319169338, 3.868676264653295949 ) ) ;
#85580=CARTESIAN_POINT ( 'NONE',  ( 4.496882872040836254, -10.53788665489624776, 3.972797206970396733 ) ) ;
#85587=CARTESIAN_POINT ( 'NONE',  ( -5.646888413699860720, -61.55025844029609772, 2.040714635159920576 ) ) ;
#85592=CARTESIAN_POINT ( 'NONE',  ( -4.472135954999577834, 249.7258814900167181, -4.000000000000002665 ) ) ;
#85603=CARTESIAN_POINT ( 'NONE',  ( 0.000000000000000000, 3.000000000000002665, 0.000000000000000000 ) ) ;
#85641=EDGE_LOOP ( 'NONE', ( #20161, #97705, #105620, #87401 ) ) ;
#85652=CARTESIAN_POINT ( 'NONE',  ( -6.944031699373469202, -9.465393454438721932, 3.972913591453822502 ) ) ;
#85666=CARTESIAN_POINT ( 'NONE',  ( 8.000113193197769590, -69.00022638645862116, -0.2613481123984630061 ) ) ;
#85741=ORIENTED_EDGE ( 'NONE', *, *, #55180, .F. ) ;
#85802=CARTESIAN_POINT ( 'NONE',  ( 7.003653396366583905, -11.05706205559678068, -3.866846144092866311 ) ) ;
#85852=CARTESIAN_POINT ( 'NONE',  ( -7.211357414135266097, -67.01146539934443069, 3.467230644691331687 ) ) ;
#85905=EDGE_CURVE ( 'NONE', #25105, #38536, #97822, .T. ) ;
#85979=CARTESIAN_POINT ( 'NONE',  ( 0.000000000000000000, -100.0000000000000000, -13.00000000000003730 ) ) ;
#85983=EDGE_CURVE ( 'NONE', #12726, #2575, #95174, .T. ) ;
#86001=DIRECTION ( 'NONE',  ( 0.000000000000000000, 0.000000000000000000, 1.000000000000000000 ) ) ;
#86127=CARTESIAN_POINT ( 'NONE',  ( -5.981691436642410764, -61.02730900805882186, -0.5384679144502715342 ) ) ;
#86145=DIRECTION ( 'NONE',  ( 1.000000000000000000, -0.000000000000000000, -0.000000000000000000 ) ) ;
#86166=CARTESIAN_POINT ( 'NONE',  ( -9.253583916535191634, 248.7019609199495846, 3.792462592445559721 ) ) ;
#86223=CARTESIAN_POINT ( 'NONE',  ( 5.982126593009819082, -6.026657721070697526, 0.5333292889181923124 ) ) ;
#86305=EDGE_LOOP ( 'NONE', ( #26761, #20948, #19160, #100638 ) ) ;
#86335=CARTESIAN_POINT ( 'NONE',  ( -4.497431761510337189, -65.54098124251032687, -3.972160586670089089 ) ) ;
#86354=FACE_BOUND ( 'NONE', #48517, .T. ) ;
#86358=CARTESIAN_POINT ( 'NONE',  ( 7.999912353029506207, -81.00017529396907889, -0.2691822806795012846 ) ) ;
#86383=CARTESIAN_POINT ( 'NONE',  ( -7.986452802927061612, -68.97309757691888876, 0.5332468218996320175 ) ) ;
#86384=ORIENTED_EDGE ( 'NONE', *, *, #87798, .F. ) ;
#86518=CYLINDRICAL_SURFACE ( 'NONE', #58133, 10.00000000000001954 ) ;
#86548=CARTESIAN_POINT ( 'NONE',  ( -5.477432325710317684, -13.16479535570474368, 2.459915882346688676 ) ) ;
#86595=DIRECTION ( 'NONE',  ( 0.000000000000000000, 0.000000000000000000, -1.000000000000000000 ) ) ;
#86635=CARTESIAN_POINT ( 'NONE',  ( 7.046289519167721060, -63.69408180055623347, -3.789821819998816288 ) ) ;
#86657=CARTESIAN_POINT ( 'NONE',  ( -5.191472769733072035, -62.35908423281053103, -3.014900733016762313 ) ) ;
#86682=CARTESIAN_POINT ( 'NONE',  ( 8.000086790516057533, -5.999826418939942840, 0.2639471549312809584 ) ) ;
#86752=EDGE_LOOP ( 'NONE', ( #73515, #89276 ) ) ;
#86829=VERTEX_POINT ( 'NONE', #42445 ) ;
#86855=CARTESIAN_POINT ( 'NONE',  ( 7.934203308536662114, -13.86700340017798183, 1.057099537198543882 ) ) ;
#86931=CARTESIAN_POINT ( 'NONE',  ( -4.567209634097059379, 250.9359978608551387, -3.891254717191793056 ) ) ;
#86975=CARTESIAN_POINT ( 'NONE',  ( 5.382954851612914204, -67.99987491489444835, -2.657971597726724866 ) ) ;
#87167=CARTESIAN_POINT ( 'NONE',  ( -6.928203230275508773, -85.26930929695541295, -4.000000000000001776 ) ) ;
#87173=CARTESIAN_POINT ( 'NONE',  ( -4.696906829037967412, -63.56001852512106609, -3.734050370377311356 ) ) ;
#87181=EDGE_LOOP ( 'NONE', ( #56054, #57924 ) ) ;
#87225=ORIENTED_EDGE ( 'NONE', *, *, #38007, .T. ) ;
#87331=VERTEX_POINT ( 'NONE', #43191 ) ;
#87346=ADVANCED_FACE ( 'NONE', ( #98227 ), #58304, .F. ) ;
#87382=CARTESIAN_POINT ( 'NONE',  ( -5.999511540169428336, -68.99926730885432846, -0.2833228702578380331 ) ) ;
#87396=AXIS2_PLACEMENT_3D ( 'NONE', #88795, #56394, #105504 ) ;
#87401=ORIENTED_EDGE ( 'NONE', *, *, #6401, .T. ) ;
#87500=CARTESIAN_POINT ( 'NONE',  ( 5.191472769733077364, -67.64091576718948318, -3.014900733016756540 ) ) ;
#87522=FACE_OUTER_BOUND ( 'NONE', #85641, .T. ) ;
#87571=CIRCLE ( 'NONE', #94507, 8.000000000000007105 ) ;
#87721=CARTESIAN_POINT ( 'NONE',  ( 0.000000000000000000, -100.0000000000000000, -8.000000000000007105 ) ) ;
#87798=EDGE_CURVE ( 'NONE', #52756, #38536, #104716, .T. ) ;
#87813=B_SPLINE_CURVE_WITH_KNOTS ( 'NONE', 3,
 ( #29865, #13632, #79441, #88081, #104243, #63276, #96176, #55151, #65389, #32517, #33049, #48649, #57271, #97733, #98795, #58356, #41643, #74527, #9257, #42167, #75050, #65916, #1146, #81533, #7658, #40577, #34121, #89668, #89134, #90729, #82085, #79, #97210, #23360, #73996, #8203 ),
 .UNSPECIFIED., .F., .F.,
 ( 4, 2, 2, 2, 2, 2, 2, 2, 2, 2, 2, 2, 2, 2, 2, 2, 2, 4 ),
 ( 0.01291936762762758983, 0.01372441420841339667, 0.01452946078919920350, 0.01533450736998501034, 0.01613955395077081717, 0.01694460053155662227, 0.01774964711234243084, 0.01855469369312823594, 0.01935974027391404451, 0.02016478685469984961, 0.02096983343548565470, 0.02177488001627146327, 0.02257992659705727184, 0.02338497317784307694, 0.02419001975862888204, 0.02459254304902178806, 0.02499506633941468714, 0.02580011292020053387 ),
 .UNSPECIFIED. ) ;
#87874=DIRECTION ( 'NONE',  ( 0.000000000000000000, 0.000000000000000000, 1.000000000000000000 ) ) ;
#88028=CARTESIAN_POINT ( 'NONE',  ( 5.981691436642412540, -68.97269099194116393, -0.5384679144502658721 ) ) ;
#88047=CARTESIAN_POINT ( 'NONE',  ( -4.660674839411965920, -8.682175146955943390, -3.778981567323763002 ) ) ;
#88052=CARTESIAN_POINT ( 'NONE',  ( 0.000000000000000000, 3.000000000000002665, 0.000000000000000000 ) ) ;
#88081=CARTESIAN_POINT ( 'NONE',  ( 4.589925132946516939, -86.06526016292519898, 3.864926970398267603 ) ) ;
#88101=CARTESIAN_POINT ( 'NONE',  ( 0.000000000000000000, 299.9999999999999432, 0.000000000000000000 ) ) ;
#88117=CARTESIAN_POINT ( 'NONE',  ( -4.472135954999580498, -10.00000000000000888, 4.000000000000000000 ) ) ;
#88119=MANIFOLD_SOLID_BREP ( 'Cut-Extrude3', #106576 ) ;
#88223=CARTESIAN_POINT ( 'NONE',  ( 4.472135954999581386, -10.00000000000000888, -4.000000000000000000 ) ) ;
#88255=CARTESIAN_POINT ( 'NONE',  ( 7.414346147791998298, -7.354108423377371473, -3.010818766110529232 ) ) ;
#88263=B_SPLINE_CURVE_WITH_KNOTS ( 'NONE', 3,
 ( #11657, #87167, #30007, #77477, #3589, #69391, #102274, #28423, #37047, #12193, #61299, #103345, #28976, #69914, #45124, #85035, #21391, #13248, #61842, #78002, #95260, #4118, #102814, #45644, #103857, #46172, #94739, #78520, #70450, #29493, #62369, #54228, #79062, #5181 ),
 .UNSPECIFIED., .F., .F.,
 ( 4, 2, 2, 2, 2, 2, 2, 2, 2, 2, 2, 2, 2, 2, 2, 2, 4 ),
 ( 0.000000000000000000, 0.0007951492273476391814, 0.001590298454695278363, 0.002385447682042917544, 0.003180596909390556726, 0.003975746136738195907, 0.004770895364085835089, 0.005566044591433473403, 0.006361193818781111717, 0.007156343046128750031, 0.007951492273476388345, 0.008746641500824025792, 0.009541790728171663238, 0.01033693995551930069, 0.01113208918286693987, 0.01192723841021457558, 0.01272238763756221476 ),
 .UNSPECIFIED. ) ;
#88325=CARTESIAN_POINT ( 'NONE',  ( 9.165151389911699198, 249.9999999999999432, 4.000000000000002665 ) ) ;
#88458=B_SPLINE_CURVE_WITH_KNOTS ( 'NONE', 3,
 ( #99302, #92823, #1672, #75027, #99848, #58881, #17895, #13481, #37283, #20600, #28662, #96020, #52902, #78233, #21111, #11353, #86358, #12423, #77178, #4349, #85269, #94441, #36230, #79291, #69627, #12951, #45871, #62596, #70149, #45355, #3289, #78751, #29210, #103054 ),
 .UNSPECIFIED., .F., .F.,
 ( 4, 2, 2, 2, 2, 2, 2, 2, 2, 2, 2, 2, 2, 2, 2, 2, 4 ),
 ( 0.000000000000000000, 0.0007951492273476391814, 0.001590298454695278363, 0.002385447682042917544, 0.003180596909390556726, 0.003975746136738195907, 0.004770895364085835089, 0.005566044591433473403, 0.006361193818781111717, 0.007156343046128750031, 0.007951492273476388345, 0.008746641500824025792, 0.009541790728171663238, 0.01033693995551930069, 0.01113208918286693987, 0.01192723841021457558, 0.01272238763756221476 ),
 .UNSPECIFIED. ) ;
#88518=EDGE_LOOP ( 'NONE', ( #13267, #16392 ) ) ;
#88616=CARTESIAN_POINT ( 'NONE',  ( 0.000000000000000000, 0.000000000000000000, -7.999999999999994671 ) ) ;
#88649=PRODUCT_CONTEXT ( 'NONE', #105855, 'mechanical' ) ;
#88680=CARTESIAN_POINT ( 'NONE',  ( -7.151217271224852290, -11.78749400445715700, -3.587901469523287368 ) ) ;
#88769=AXIS2_PLACEMENT_3D ( 'NONE', #10591, #27370, #99599 ) ;
#88795=CARTESIAN_POINT ( 'NONE',  ( 0.000000000000000000, 3.000000000000002665, 0.000000000000000000 ) ) ;
#88811=CARTESIAN_POINT ( 'NONE',  ( -8.000113193197767814, -80.99977361354137884, -0.2613481123984638943 ) ) ;
#88825=CARTESIAN_POINT ( 'NONE',  ( 0.000000000000000000, 1.000000000000000888, 0.000000000000000000 ) ) ;
#88910=EDGE_CURVE ( 'NONE', #28004, #87331, #88263, .T. ) ;
#88924=CARTESIAN_POINT ( 'NONE',  ( 0.000000000000000000, 300.0000000000000568, 0.000000000000000000 ) ) ;
#88961=CARTESIAN_POINT ( 'NONE',  ( -6.000469943554648466, -69.00070491670500417, 0.2622423038614459245 ) ) ;
#89134=CARTESIAN_POINT ( 'NONE',  ( 4.814352310392316703, -86.79678594103579314, -3.583053941560736089 ) ) ;
#89137=ADVANCED_FACE ( 'NONE', ( #37315 ), #12979, .F. ) ;
#89163=CARTESIAN_POINT ( 'NONE',  ( 7.934996450857311423, -88.86862456472529459, -1.050865690281774345 ) ) ;
#89172=AXIS2_PLACEMENT_3D ( 'NONE', #46474, #37889, #69698 ) ;
#89178=VERTEX_POINT ( 'NONE', #103083 ) ;
#89214=CARTESIAN_POINT ( 'NONE',  ( -7.744991119775241017, -13.46438785425130824, -2.016316005557097224 ) ) ;
#89276=ORIENTED_EDGE ( 'NONE', *, *, #14871, .T. ) ;
#89310=CARTESIAN_POINT ( 'NONE',  ( 9.989113211954187221, 246.0270072645100470, 0.5334031035449080527 ) ) ;
#89345=EDGE_CURVE ( 'NONE', #33707, #76918, #25835, .T. ) ;
#89393=CARTESIAN_POINT ( 'NONE',  ( 5.477432325710314132, -6.835204644295279408, 2.459915882346691340 ) ) ;
#89413=VECTOR ( 'NONE', #67522, 1000.000000000000000 ) ;
#89438=DIRECTION ( 'NONE',  ( 1.224646799147351482E-16, 0.000000000000000000, -1.000000000000000000 ) ) ;
#89448=EDGE_CURVE ( 'NONE', #87331, #4789, #83562, .T. ) ;
#89659=CIRCLE ( 'NONE', #12111, 12.00000000000003908 ) ;
#89668=CARTESIAN_POINT ( 'NONE',  ( 4.905018583967755141, -87.02359985679682097, -3.459768807258293055 ) ) ;
#89705=B_SPLINE_CURVE_WITH_KNOTS ( 'NONE', 3,
 ( #21722, #6021, #20691, #63756, #54032, #104188, #70246, #37386, #94540, #13581, #4984, #78854, #79389, #95067, #103669, #103148, #38432, #104725, #88028, #14107, #55617, #5507, #21202, #14633, #86975, #87500, #47542, #13046, #30878, #47013, #38946, #45976, #80440, #71823, #37912, #29816 ),
 .UNSPECIFIED., .F., .F.,
 ( 4, 2, 2, 2, 2, 2, 2, 2, 2, 2, 2, 2, 2, 2, 2, 2, 2, 4 ),
 ( 0.01291936762762759677, 0.01372441420841340708, 0.01452946078919921911, 0.01533450736998502942, 0.01613955395077084146, 0.01694460053155665349, 0.01774964711234246206, 0.01855469369312827410, 0.01935974027391408614, 0.02016478685469989818, 0.02096983343548571022, 0.02177488001627151878, 0.02257992659705733082, 0.02338497317784313939, 0.02419001975862895143, 0.02459254304902185745, 0.02499506633941476347, 0.02580011292020053387 ),
 .UNSPECIFIED. ) ;
#89762=EDGE_LOOP ( 'NONE', ( #41310, #66522, #406, #48756 ) ) ;
#89828=AXIS2_PLACEMENT_3D ( 'NONE', #91994, #102751, #86595 ) ;
#89923=ORIENTED_EDGE ( 'NONE', *, *, #37911, .F. ) ;
#89979=CARTESIAN_POINT ( 'NONE',  ( 5.909259836070535954, -81.13722795757931294, -1.072443315311454981 ) ) ;
#90114=( GEOMETRIC_REPRESENTATION_CONTEXT ( 3 ) GLOBAL_UNCERTAINTY_ASSIGNED_CONTEXT ( ( #6786 ) ) GLOBAL_UNIT_ASSIGNED_CONTEXT ( ( #63979, #34814, #76288 ) ) REPRESENTATION_CONTEXT ( 'NONE', 'WORKASPACE' ) );
#90116=CARTESIAN_POINT ( 'NONE',  ( -4.656749229489884456, -86.31760408126429240, -3.785628640239149689 ) ) ;
#90219=CARTESIAN_POINT ( 'NONE',  ( 7.619753052866895970, -88.17451502807176666, -2.447276542590447246 ) ) ;
#90226=CIRCLE ( 'NONE', #74727, 13.00000000000003730 ) ;
#90407=CARTESIAN_POINT ( 'NONE',  ( -6.944371705245973025, -84.46100308575455529, -3.972324460300566962 ) ) ;
#90413=CARTESIAN_POINT ( 'NONE',  ( -9.646032546913161809, 253.0128032847436828, 2.644051433538248119 ) ) ;
#90524=ORIENTED_EDGE ( 'NONE', *, *, #38007, .F. ) ;
#90538=SURFACE_STYLE_USAGE ( .BOTH. , #47408 ) ;
#90651=CARTESIAN_POINT ( 'NONE',  ( -5.728413875956868573, -88.58064226453400636, 1.802282772585248605 ) ) ;
#90680=CARTESIAN_POINT ( 'NONE',  ( -7.934996450857313199, -61.13137543527469830, -1.050865690281778120 ) ) ;
#90729=CARTESIAN_POINT ( 'NONE',  ( 4.696906829037973630, -86.43998147487897654, -3.734050370377307360 ) ) ;
#90734=CARTESIAN_POINT ( 'NONE',  ( -6.943926999490789953, -65.53300992626145671, -3.973092371898546915 ) ) ;
#90898=B_SPLINE_CURVE_WITH_KNOTS ( 'NONE', 3,
 ( #81464, #18375, #10768, #37231, #18927, #19467, #28080, #2689, #70092, #3774, #100856, #76574, #92766, #102996, #28610, #77661, #61493, #44231, #11841, #36178, #4296, #102463, #12373, #44772, #35640, #62027, #36709, #3234, #27556, #69046, #29155, #27015, #101402, #43164 ),
 .UNSPECIFIED., .F., .F.,
 ( 4, 2, 2, 2, 2, 2, 2, 2, 2, 2, 2, 2, 2, 2, 2, 2, 4 ),
 ( 0.000000000000000000, 0.0007899309203816051251, 0.001579861840763210250, 0.002369792761144815484, 0.003159723681526420500, 0.003949654601908025517, 0.004739585522289630967, 0.005529516442671235550, 0.006319447363052841000, 0.007109378283434446451, 0.007899309203816051034, 0.008689240124197656484, 0.009479171044579261934, 0.01026910196496086738, 0.01105903288534247110, 0.01184896380572407655, 0.01263889472610568200 ),
 .UNSPECIFIED. ) ;
#90949=CARTESIAN_POINT ( 'NONE',  ( -7.551560007654698481, -81.99089648193009339, -2.648022159607833270 ) ) ;
#91012=VECTOR ( 'NONE', #76531, 1000.000000000000000 ) ;
#91040=CARTESIAN_POINT ( 'NONE',  ( 6.928203230275507885, -65.00000000000000000, 4.000000000000002665 ) ) ;
#91062=CARTESIAN_POINT ( 'NONE',  ( 4.472135954999579610, -85.00000000000000000, 4.000000000000001776 ) ) ;
#91068=EDGE_LOOP ( 'NONE', ( #51113, #17474 ) ) ;
#91230=CARTESIAN_POINT ( 'NONE',  ( -7.551892080562056186, -61.99012297460618726, 2.647003822403979356 ) ) ;
#91303=CARTESIAN_POINT ( 'NONE',  ( -5.094000037296072314, 252.4463412377122609, -3.174960020027671970 ) ) ;
#91370=CARTESIAN_POINT ( 'NONE',  ( 4.472135954999579610, 249.9999999999999716, -4.000000000000002665 ) ) ;
#91441=CARTESIAN_POINT ( 'NONE',  ( 9.334514330295450080, 248.2137726231820523, -3.588704711590614771 ) ) ;
#91444=CARTESIAN_POINT ( 'NONE',  ( 7.150053860865849487, -8.217345460860238759, 3.590189269391289351 ) ) ;
#91487=CARTESIAN_POINT ( 'NONE',  ( -9.989690267985819716, 253.9744441659491088, -0.5238310916885637880 ) ) ;
#91538=CARTESIAN_POINT ( 'NONE',  ( 4.567209634097052273, -10.93599786085512804, -3.891254717191802381 ) ) ;
#91551=CARTESIAN_POINT ( 'NONE',  ( -4.813555570991618460, 248.2052620348266601, -3.584128953194777534 ) ) ;
#91588=CARTESIAN_POINT ( 'NONE',  ( 4.656749229489884456, -83.68239591873569339, -3.785628640239149689 ) ) ;
#91725=FACE_OUTER_BOUND ( 'NONE', #91068, .T. ) ;
#91740=ORIENTED_EDGE ( 'NONE', *, *, #48782, .T. ) ;
#91742=DIRECTION ( 'NONE',  ( -0.000000000000000000, -1.000000000000000000, -0.000000000000000000 ) ) ;
#91994=CARTESIAN_POINT ( 'NONE',  ( -13.00000000000003730, -85.00000000000000000, 0.000000000000000000 ) ) ;
#92001=CARTESIAN_POINT ( 'NONE',  ( -9.843481099141484947, 253.5920455615338653, -1.779148000612170488 ) ) ;
#92056=ORIENTED_EDGE ( 'NONE', *, *, #54602, .F. ) ;
#92061=CARTESIAN_POINT ( 'NONE',  ( -5.093234209761986264, 247.5553222653508669, 3.176141468578064675 ) ) ;
#92123=CARTESIAN_POINT ( 'NONE',  ( -7.413471587080150194, -7.356478408316738715, -3.013058070223549656 ) ) ;
#92152=CARTESIAN_POINT ( 'NONE',  ( 4.472135954999579610, 249.9999999999999716, -4.000000000000002665 ) ) ;
#92167=ORIENTED_EDGE ( 'NONE', *, *, #100922, .T. ) ;
#92252=CARTESIAN_POINT ( 'NONE',  ( -7.413471587080153746, -62.35647840831676092, -3.013058070223552765 ) ) ;
#92428=ORIENTED_EDGE ( 'NONE', *, *, #56018, .T. ) ;
#92430=CIRCLE ( 'NONE', #101065, 6.000000000000000888 ) ;
#92471=SHAPE_REPRESENTATION_RELATIONSHIP ( 'NONE' , 'NONE' ,  #84690, #101356 ) ;
#92478=CARTESIAN_POINT ( 'NONE',  ( 9.918512371096317892, 246.2071700772944780, -1.297150762882707031 ) ) ;
#92528=CARTESIAN_POINT ( 'NONE',  ( 5.725004243152318928, 253.5751914825536346, -1.812899781754669259 ) ) ;
#92573=CARTESIAN_POINT ( 'NONE',  ( -5.191472769733078252, -82.35908423281054525, -3.014900733016756540 ) ) ;
#92577=VERTEX_POINT ( 'NONE', #91370 ) ;
#92583=CARTESIAN_POINT ( 'NONE',  ( 5.981691436642411652, -13.97269099194115860, -0.5384679144502718673 ) ) ;
#92603=CARTESIAN_POINT ( 'NONE',  ( 7.344133061198927948, -87.44494392680577732, 3.176267128233875248 ) ) ;
#92659=CARTESIAN_POINT ( 'NONE',  ( -8.000113193197769590, -5.999773613541393047, -0.2613481123984661703 ) ) ;
#92766=CARTESIAN_POINT ( 'NONE',  ( 9.843039827103257977, 253.5908350250832939, -1.781495459429556893 ) ) ;
#92774=FACE_BOUND ( 'NONE', #6771, .T. ) ;
#92797=CARTESIAN_POINT ( 'NONE',  ( 7.744329845603314944, -13.46288230153455778, -2.018701143083234673 ) ) ;
#92823=CARTESIAN_POINT ( 'NONE',  ( 6.928203230275508773, -84.73069070304464390, -4.000000000000001776 ) ) ;
#92871=CARTESIAN_POINT ( 'NONE',  ( -5.725989721596485005, 253.5767711125646713, 1.809923354557167352 ) ) ;
#92940=CARTESIAN_POINT ( 'NONE',  ( -5.191472769733075587, -7.359084232810527482, -3.014900733016758760 ) ) ;
#93020=CARTESIAN_POINT ( 'NONE',  ( 9.646083234704185827, 246.9870939097651785, -2.643797197754298889 ) ) ;
#93072=CARTESIAN_POINT ( 'NONE',  ( 5.192560085536420900, 252.6430544263124034, 3.013051918867540202 ) ) ;
#93096=UNCERTAINTY_MEASURE_WITH_UNIT (LENGTH_MEASURE( 1.000000000000000082E-05 ), #4142, 'distance_accuracy_value', 'NONE');
#93103=CARTESIAN_POINT ( 'NONE',  ( 7.744991119775239241, -61.53561214574870775, -2.016316005557097668 ) ) ;
#93110=CARTESIAN_POINT ( 'NONE',  ( -4.814352310392316703, -83.20321405896427791, -3.583053941560736089 ) ) ;
#93121=CARTESIAN_POINT ( 'NONE',  ( 5.382954851612913316, -12.99987491489446434, -2.657971597726729307 ) ) ;
#93129=CARTESIAN_POINT ( 'NONE',  ( -4.472135954999578722, -65.00000000000000000, -4.000000000000002665 ) ) ;
#93135=CARTESIAN_POINT ( 'NONE',  ( -5.093082057083965886, 247.5555379357842298, -3.176439207277718779 ) ) ;
#93145=CARTESIAN_POINT ( 'NONE',  ( 7.934203308536662114, -88.86700340017800670, 1.057099537198545214 ) ) ;
#93156=ADVANCED_FACE ( 'NONE', ( #47440, #86354, #70145, #103050 ), #62079, .T. ) ;
#93169=CARTESIAN_POINT ( 'NONE',  ( -9.644834624769993425, 246.9910949979422128, 2.648308524638419925 ) ) ;
#93213=CARTESIAN_POINT ( 'NONE',  ( 7.744168461338431619, -68.46254061715158912, 2.019395720771554270 ) ) ;
#93227=CARTESIAN_POINT ( 'NONE',  ( 4.656749229489888897, -8.682395918735693385, -3.785628640239143472 ) ) ;
#93229=CARTESIAN_POINT ( 'NONE',  ( 5.382954851612907987, 247.0001250851054522, -2.657971597726739965 ) ) ;
#93317=CARTESIAN_POINT ( 'NONE',  ( 0.000000000000000000, 0.000000000000000000, -13.00000000000003730 ) ) ;
#93337=DIRECTION ( 'NONE',  ( 0.000000000000000000, 0.000000000000000000, -1.000000000000000000 ) ) ;
#93399=ORIENTED_EDGE ( 'NONE', *, *, #32427, .F. ) ;
#93564=CARTESIAN_POINT ( 'NONE',  ( 9.948688207305211861, 246.1297685050980704, -1.044946705213434690 ) ) ;
#93586=AXIS2_PLACEMENT_3D ( 'NONE', #97491, #98040, #24190 ) ;
#93604=EDGE_CURVE ( 'NONE', #41649, #65228, #32636, .T. ) ;
#93611=LINE ( 'NONE', #36474, #37848 ) ;
#93645=CARTESIAN_POINT ( 'NONE',  ( 7.002619243997878939, -63.94992681986182248, -3.868708944013000917 ) ) ;
#93662=CARTESIAN_POINT ( 'NONE',  ( 4.472135954999581386, -10.27077220067364749, 4.000000000000000888 ) ) ;
#93669=CARTESIAN_POINT ( 'NONE',  ( -4.814352310392309597, -63.20321405896424238, -3.583053941560743194 ) ) ;
#93674=CARTESIAN_POINT ( 'NONE',  ( -5.858881034796409537, 246.2141367599701312, 1.317748741875975682 ) ) ;
#93733=CARTESIAN_POINT ( 'NONE',  ( -7.551560007654697593, -6.990896481930088946, -2.648022159607835491 ) ) ;
#93763=CARTESIAN_POINT ( 'NONE',  ( 5.475947152006322760, 246.8378226989086954, 2.462898245435130029 ) ) ;
#93868=CARTESIAN_POINT ( 'NONE',  ( 4.472135954999578722, -65.00000000000000000, -4.000000000000002665 ) ) ;
#93872=CARTESIAN_POINT ( 'NONE',  ( -5.909259836070535066, -68.86277204242070127, -1.072443315311455647 ) ) ;
#93889=B_SPLINE_CURVE_WITH_KNOTS ( 'NONE', 3,
 ( #76953, #61326, #46575, #35474, #59728, #21805, #54645, #92603, #18759, #76413, #68344, #101242, #27396, #60277, #93145, #11135, #68889, #101762, #60795, #89163, #16323, #56225, #39030, #90219, #64369, #15268, #105863, #48151, #81050, #57300, #64880, #73485, #15797, #49214 ),
 .UNSPECIFIED., .F., .F.,
 ( 4, 2, 2, 2, 2, 2, 2, 2, 2, 2, 2, 2, 2, 2, 2, 2, 4 ),
 ( 0.01272238763756221476, 0.01351613129786393384, 0.01430987495816565119, 0.01510361861846737028, 0.01589736227876908936, 0.01669110593907080844, 0.01748484959937252753, 0.01827859325967424314, 0.01907233691997596223, 0.01986608058027768131, 0.02065982424057940040, 0.02145356790088111948, 0.02224731156118283509, 0.02304105522148455765, 0.02383479888178627326, 0.02462854254208799235, 0.02542228620238971143 ),
 .UNSPECIFIED. ) ;
#93923=CARTESIAN_POINT ( 'NONE',  ( -7.934883677559682269, -68.86839177937554268, 1.051380792122688757 ) ) ;
#94152=EDGE_CURVE ( 'NONE', #89178, #49420, #21122, .T. ) ;
#94180=CARTESIAN_POINT ( 'NONE',  ( -5.999787407977321685, -81.00031888815553316, 0.2740427891043037412 ) ) ;
#94197=CARTESIAN_POINT ( 'NONE',  ( -4.472135954999578722, -65.00000000000000000, 4.000000000000002665 ) ) ;
#94300=CARTESIAN_POINT ( 'NONE',  ( 5.858824175751778718, 246.2142093912763698, -1.318356988357147097 ) ) ;
#94313=B_SPLINE_CURVE_WITH_KNOTS ( 'NONE', 3,
 ( #60757, #12171, #4099, #93645, #86635, #2482, #60235, #101197, #27356, #45103, #19793, #93103, #61825, #35974, #18715, #52627, #19275, #52103, #37027, #85012, #11096, #69896, #44021, #84485, #76914, #69372, #27890, #3024, #36505, #68846, #85560, #102794, #11635, #44568 ),
 .UNSPECIFIED., .F., .F.,
 ( 4, 2, 2, 2, 2, 2, 2, 2, 2, 2, 2, 2, 2, 2, 2, 2, 4 ),
 ( 0.000000000000000000, 0.0007951492273476290984, 0.001590298454695258197, 0.002385447682042887187, 0.003180596909390516393, 0.003975746136738159478, 0.004770895364085802996, 0.005566044591433445647, 0.006361193818781088298, 0.007156343046128731816, 0.007951492273476374467, 0.008746641500824017118, 0.009541790728171658034, 0.01033693995551929895, 0.01113208918286694160, 0.01192723841021458425, 0.01272238763756222690 ),
 .UNSPECIFIED. ) ;
#94382=DIRECTION ( 'NONE',  ( 1.000000000000000000, -0.000000000000000000, -0.000000000000000000 ) ) ;
#94386=CARTESIAN_POINT ( 'NONE',  ( 1.469576158976828483E-15, 1.000000000000000888, 12.00000000000003908 ) ) ;
#94416=CARTESIAN_POINT ( 'NONE',  ( 7.213352437320217803, -12.01836473007682038, -3.463014597543478068 ) ) ;
#94441=CARTESIAN_POINT ( 'NONE',  ( 7.800703710507056243, -81.41404307342060065, 1.791736796405269061 ) ) ;
#94465=CARTESIAN_POINT ( 'NONE',  ( -7.002641335706725201, -66.05087262680832794, 3.868676264653295949 ) ) ;
#94507=AXIS2_PLACEMENT_3D ( 'NONE', #106489, #80620, #71470 ) ;
#94540=CARTESIAN_POINT ( 'NONE',  ( 5.191144708981716427, -67.64030085521270053, 3.015512395308852067 ) ) ;
#94561=CARTESIAN_POINT ( 'NONE',  ( -6.000208918519487789, -5.999686622100329991, -0.2646532170642320048 ) ) ;
#94599=DIRECTION ( 'NONE',  ( -0.000000000000000000, -1.000000000000000000, -0.000000000000000000 ) ) ;
#94625=VERTEX_POINT ( 'NONE', #51318 ) ;
#94633=CARTESIAN_POINT ( 'NONE',  ( -5.382057749264597568, -12.99826798403944572, -2.659775980967104658 ) ) ;
#94739=CARTESIAN_POINT ( 'NONE',  ( -7.343637806710343163, -87.44363121900614999, 3.177475076494674866 ) ) ;
#94761=( NAMED_UNIT ( * ) PLANE_ANGLE_UNIT ( ) SI_UNIT ( $, .RADIAN. ) );
#94770=AXIS2_PLACEMENT_3D ( 'NONE', #5636, #45586, #13183 ) ;
#94824=CARTESIAN_POINT ( 'NONE',  ( 7.801642220026309360, -68.58796826149033166, 1.787233835843584862 ) ) ;
#94887=ORIENTED_EDGE ( 'NONE', *, *, #63054, .F. ) ;
#94926=ORIENTED_EDGE ( 'NONE', *, *, #72594, .F. ) ;
#94952=CARTESIAN_POINT ( 'NONE',  ( 7.999885325681428405, -13.99977065129938048, 0.2682325777720028781 ) ) ;
#95067=CARTESIAN_POINT ( 'NONE',  ( 5.856955515201464735, -68.78289058880862683, 1.326217528971463055 ) ) ;
#95097=CARTESIAN_POINT ( 'NONE',  ( -13.00000000000003730, -85.00000000000000000, -4.000000000000001776 ) ) ;
#95169=DIRECTION ( 'NONE',  ( 0.000000000000000000, 0.000000000000000000, 1.000000000000000000 ) ) ;
#95174=B_SPLINE_CURVE_WITH_KNOTS ( 'NONE', 3,
 ( #60985, #102496, #86335, #44261, #28640, #101951, #77153, #44803, #70123, #12931, #77692, #3268, #36209, #69076, #93872, #72756, #87382, #88961, #37795, #30213, #56572, #105663, #21604, #54435, #31799, #23183, #13459, #95999, #5393, #15591, #47946, #97042, #80852, #79800, #48482, #54976 ),
 .UNSPECIFIED., .F., .F.,
 ( 4, 2, 2, 2, 2, 2, 2, 2, 2, 2, 2, 2, 2, 2, 2, 2, 2, 4 ),
 ( 0.000000000000000000, 0.0008074604767267247983, 0.001614920953453449597, 0.002422381430180174395, 0.003229841906906899193, 0.004037302383633624425, 0.004844762860360348790, 0.005652223337087073154, 0.006459683813813798386, 0.007267144290540523618, 0.008074604767267248850, 0.008882065243993972348, 0.009689525720720697580, 0.01049698619744742281, 0.01130444667417414631, 0.01211190715090087154, 0.01251563738926423502, 0.01291936762762759677 ),
 .UNSPECIFIED. ) ;
#95260=CARTESIAN_POINT ( 'NONE',  ( -7.896571385775229324, -88.78997999345754977, 1.305932416347435732 ) ) ;
#95295=( GEOMETRIC_REPRESENTATION_CONTEXT ( 3 ) GLOBAL_UNCERTAINTY_ASSIGNED_CONTEXT ( ( #27668 ) ) GLOBAL_UNIT_ASSIGNED_CONTEXT ( ( #101104, #59061, #9960 ) ) REPRESENTATION_CONTEXT ( 'NONE', 'WORKASPACE' ) );
#95323=VECTOR ( 'NONE', #94382, 1000.000000000000000 ) ;
#95331=SURFACE_SIDE_STYLE ('',( #30082 ) ) ;
#95425=CARTESIAN_POINT ( 'NONE',  ( 5.093082057083964997, -62.55553793578429378, -3.176439207277723664 ) ) ;
#95454=B_SPLINE_CURVE_WITH_KNOTS ( 'NONE', 3,
 ( #94197, #44593, #61306, #54233, #68874, #62375, #20366, #60261, #76939, #53207, #4658, #85587, #36532, #12727, #19821, #61848, #3595, #103352, #86127, #29500, #12199, #11123, #78007, #4124, #27917, #86657, #37053, #60780, #93669, #87173, #102821, #53729, #27381, #70455, #28982, #93129 ),
 .UNSPECIFIED., .F., .F.,
 ( 4, 2, 2, 2, 2, 2, 2, 2, 2, 2, 2, 2, 2, 2, 2, 2, 2, 4 ),
 ( 0.01291936762762759677, 0.01372441420841340881, 0.01452946078919922085, 0.01533450736998503289, 0.01613955395077084493, 0.01694460053155665696, 0.01774964711234246900, 0.01855469369312828104, 0.01935974027391408961, 0.02016478685469990165, 0.02096983343548571369, 0.02177488001627152572, 0.02257992659705733776, 0.02338497317784314633, 0.02419001975862895837, 0.02459254304902186439, 0.02499506633941477041, 0.02580011292020054428 ),
 .UNSPECIFIED. ) ;
#95476=PRESENTATION_STYLE_ASSIGNMENT (( #36225 ) ) ;
#95519=CARTESIAN_POINT ( 'NONE',  ( 1.224646799147355426E-15, -100.0000000000000000, 10.00000000000001954 ) ) ;
#95671=CARTESIAN_POINT ( 'NONE',  ( -4.903871675326606727, -12.02085807301495457, -3.461400506969853907 ) ) ;
#95701=MECHANICAL_DESIGN_GEOMETRIC_PRESENTATION_REPRESENTATION('',(#2601),#880);
#95819=CARTESIAN_POINT ( 'NONE',  ( 6.943926999490789953, -9.466990073738530853, -3.973092371898544251 ) ) ;
#95950=VECTOR ( 'NONE', #22241, 1000.000000000000000 ) ;
#95999=CARTESIAN_POINT ( 'NONE',  ( -4.905194654929172948, -67.02394395019842932, 3.459476078998854121 ) ) ;
#96020=CARTESIAN_POINT ( 'NONE',  ( 7.744991119775235688, -81.53561214574868643, -2.016316005557098112 ) ) ;
#96052=CARTESIAN_POINT ( 'NONE',  ( -13.00000000000003730, -85.00000000000000000, 0.000000000000000000 ) ) ;
#96058=CARTESIAN_POINT ( 'NONE',  ( -13.00000000000003730, -65.00000000000000000, 0.000000000000000000 ) ) ;
#96087=ORIENTED_EDGE ( 'NONE', *, *, #2564, .F. ) ;
#96176=CARTESIAN_POINT ( 'NONE',  ( 4.904566723942682671, -87.02242702470746849, 3.460360782932704549 ) ) ;
#96215=CARTESIAN_POINT ( 'NONE',  ( -5.999511540169428336, -13.99926730885433557, -0.2833228702578364788 ) ) ;
#96261=CARTESIAN_POINT ( 'NONE',  ( -7.801339272325197527, -13.58731471959700521, -1.788609912539669944 ) ) ;
#96309=ORIENTED_EDGE ( 'NONE', *, *, #43375, .T. ) ;
#96336=AXIS2_PLACEMENT_3D ( 'NONE', #11347, #12418, #61006 ) ;
#96343=DIRECTION ( 'NONE',  ( -0.000000000000000000, -1.000000000000000000, -0.000000000000000000 ) ) ;
#96375=FACE_OUTER_BOUND ( 'NONE', #85328, .T. ) ;
#96426=CARTESIAN_POINT ( 'NONE',  ( 4.658465013329191606, -8.676361203269085109, 3.783534922165391112 ) ) ;
#96498=CARTESIAN_POINT ( 'NONE',  ( 4.521127550501229386, -64.32389759472336266, 3.944701057164355706 ) ) ;
#96507=EDGE_LOOP ( 'NONE', ( #97327, #69593, #35568, #102276 ) ) ;
#96674=LINE ( 'NONE', #95097, #71904 ) ;
#96716=FACE_OUTER_BOUND ( 'NONE', #43528, .T. ) ;
#96871=CARTESIAN_POINT ( 'NONE',  ( 7.619701877737481865, -6.825578404672334898, -2.447562251315978710 ) ) ;
#96908=CARTESIAN_POINT ( 'NONE',  ( -6.928203230275508773, -85.00000000000000000, 4.000000000000001776 ) ) ;
#96920=FACE_OUTER_BOUND ( 'NONE', #86305, .T. ) ;
#96982=ORIENTED_EDGE ( 'NONE', *, *, #15652, .T. ) ;
#97027=( LENGTH_UNIT ( ) NAMED_UNIT ( * ) SI_UNIT ( .MILLI., .METRE. ) );
#97042=CARTESIAN_POINT ( 'NONE',  ( -4.521127550501226722, -65.67610240527666576, 3.944701057164355706 ) ) ;
#97102=FACE_OUTER_BOUND ( 'NONE', #38441, .T. ) ;
#97123=DIRECTION ( 'NONE',  ( 1.000000000000000000, -0.000000000000000000, -0.000000000000000000 ) ) ;
#97210=CARTESIAN_POINT ( 'NONE',  ( 4.567209634097050497, -85.93599786085513870, -3.891254717191802381 ) ) ;
#97245=AXIS2_PLACEMENT_3D ( 'NONE', #30554, #63453, #98315 ) ;
#97327=ORIENTED_EDGE ( 'NONE', *, *, #77181, .F. ) ;
#97365=ORIENTED_EDGE ( 'NONE', *, *, #13566, .T. ) ;
#97377=CARTESIAN_POINT ( 'NONE',  ( 9.699121749566376849, 246.8233123972417786, 2.444499528233566199 ) ) ;
#97393=( NAMED_UNIT ( * ) SI_UNIT ( $, .STERADIAN. ) SOLID_ANGLE_UNIT ( ) );
#97412=CARTESIAN_POINT ( 'NONE',  ( -7.986468734911285949, -81.02686320276920640, 0.5341897780976099241 ) ) ;
#97454=CARTESIAN_POINT ( 'NONE',  ( 4.815811321232739139, -8.199232923026272601, 3.581116321197040708 ) ) ;
#97491=CARTESIAN_POINT ( 'NONE',  ( 0.000000000000000000, 0.000000000000000000, 0.000000000000000000 ) ) ;
#97574=DIRECTION ( 'NONE',  ( -0.000000000000000000, -1.000000000000000000, -0.000000000000000000 ) ) ;
#97694=VECTOR ( 'NONE', #100002, 1000.000000000000000 ) ;
#97705=ORIENTED_EDGE ( 'NONE', *, *, #48755, .F. ) ;
#97733=CARTESIAN_POINT ( 'NONE',  ( 5.856955515201466511, -88.78289058880865525, 1.326217528971465942 ) ) ;
#97755=AXIS2_PLACEMENT_3D ( 'NONE', #47777, #6803, #31643 ) ;
#97822=B_SPLINE_CURVE_WITH_KNOTS ( 'NONE', 3,
 ( #59932, #52872, #45331, #4326, #20031, #27046, #3801, #61523, #62063, #103031, #10799, #12400, #67998, #60466, #86855, #68546, #94952, #51801, #43717, #21087, #53416, #36740, #92797, #78725, #100883, #76607, #2721, #94416, #18958, #35668, #85802, #101433, #78212, #53924 ),
 .UNSPECIFIED., .F., .F.,
 ( 4, 2, 2, 2, 2, 2, 2, 2, 2, 2, 2, 2, 2, 2, 2, 2, 4 ),
 ( 0.01272238763756220782, 0.01351613129786392517, 0.01430987495816564252, 0.01510361861846735987, 0.01589736227876907895, 0.01669110593907079457, 0.01748484959937251365, 0.01827859325967422927, 0.01907233691997594835, 0.01986608058027766396, 0.02065982424057938305, 0.02145356790088109866, 0.02224731156118281775, 0.02304105522148453683, 0.02383479888178625244, 0.02462854254208796806, 0.02542228620238968714 ),
 .UNSPECIFIED. ) ;
#97845=CARTESIAN_POINT ( 'NONE',  ( 0.000000000000000000, 299.9999999999999432, 0.000000000000000000 ) ) ;
#97874=ADVANCED_FACE ( 'NONE', ( #71502 ), #13794, .T. ) ;
#97911=AXIS2_PLACEMENT_3D ( 'NONE', #96052, #45907, #104658 ) ;
#97919=CARTESIAN_POINT ( 'NONE',  ( 7.002641335706727865, -8.949127373191689827, 3.868676264653292840 ) ) ;
#97965=CARTESIAN_POINT ( 'NONE',  ( -9.334514330295453632, 251.7862273768178909, -3.588704711590601004 ) ) ;
#98036=VECTOR ( 'NONE', #2656, 1000.000000000000000 ) ;
#98040=DIRECTION ( 'NONE',  ( -0.000000000000000000, -1.000000000000000000, -0.000000000000000000 ) ) ;
#98067=DIRECTION ( 'NONE',  ( -0.000000000000000000, -1.000000000000000000, -0.000000000000000000 ) ) ;
#98099=EDGE_LOOP ( 'NONE', ( #15246, #96982, #69854, #32303 ) ) ;
#98201=CARTESIAN_POINT ( 'NONE',  ( -4.503026011213025370, -85.54341862283318676, 3.965236350746919047 ) ) ;
#98227=FACE_OUTER_BOUND ( 'NONE', #1751, .T. ) ;
#98228=CARTESIAN_POINT ( 'NONE',  ( -7.002990960197235104, -63.94733181616542339, 3.868040364119525343 ) ) ;
#98283=MECHANICAL_DESIGN_GEOMETRIC_PRESENTATION_REPRESENTATION('',(#38036),#34568);
#98315=DIRECTION ( 'NONE',  ( 0.000000000000000000, 0.000000000000000000, -1.000000000000000000 ) ) ;
#98461=SURFACE_STYLE_USAGE ( .BOTH. , #32707 ) ;
#98482=CARTESIAN_POINT ( 'NONE',  ( -7.801777176595948937, -81.41172014187365846, -1.786991866639921822 ) ) ;
#98591=CARTESIAN_POINT ( 'NONE',  ( 4.497431761510337189, -84.45901875748972998, -3.972160586670088200 ) ) ;
#98637=ORIENTED_EDGE ( 'NONE', *, *, #89345, .F. ) ;
#98746=CARTESIAN_POINT ( 'NONE',  ( -6.928203230275509661, -65.00000000000000000, -4.000000000000002665 ) ) ;
#98795=CARTESIAN_POINT ( 'NONE',  ( 5.909155701201243893, -88.86261680188731304, 1.073778020691686486 ) ) ;
#98891=EDGE_CURVE ( 'NONE', #54176, #4111, #48162, .T. ) ;
#98988=ORIENTED_EDGE ( 'NONE', *, *, #73802, .F. ) ;
#99002=CARTESIAN_POINT ( 'NONE',  ( -7.151597709147949011, -83.21070734947784331, 3.587174531012140566 ) ) ;
#99098=B_SPLINE_CURVE_WITH_KNOTS ( 'NONE', 3,
 ( #82091, #74000, #90734, #16850, #8739, #53464, #3313, #35178, #70175, #20622, #102001, #37312, #52926, #103080, #43768, #35721, #77204, #29232, #86383, #93923, #43246, #78259, #76659, #4371, #60513, #36259, #28160, #85852, #61573, #76131, #94465, #61035, #62109, #3853 ),
 .UNSPECIFIED., .F., .F.,
 ( 4, 2, 2, 2, 2, 2, 2, 2, 2, 2, 2, 2, 2, 2, 2, 2, 4 ),
 ( 0.000000000000000000, 0.0007951492273476392899, 0.001590298454695278580, 0.002385447682042917544, 0.003180596909390557159, 0.003975746136738196775, 0.004770895364085835089, 0.005566044591433475137, 0.006361193818781114319, 0.007156343046128752633, 0.007951492273476393549, 0.008746641500824030996, 0.009541790728171668443, 0.01033693995551930589, 0.01113208918286694334, 0.01192723841021458252, 0.01272238763756221996 ),
 .UNSPECIFIED. ) ;
#99249=CARTESIAN_POINT ( 'NONE',  ( -5.647817967127097383, -88.45126406528795826, -2.038183545141173614 ) ) ;
#99255=FACE_BOUND ( 'NONE', #7460, .T. ) ;
#99273=CARTESIAN_POINT ( 'NONE',  ( -7.986711519608431509, -61.02638096376566779, -0.5300249774147625104 ) ) ;
#99302=CARTESIAN_POINT ( 'NONE',  ( 6.928203230275507885, -85.00000000000000000, -4.000000000000001776 ) ) ;
#99348=CARTESIAN_POINT ( 'NONE',  ( -5.382954851612910652, 252.9998749148943489, -2.657971597726735524 ) ) ;
#99363=AXIS2_PLACEMENT_3D ( 'NONE', #45688, #37635, #54272 ) ;
#99489=FILL_AREA_STYLE ('',( #67681 ) ) ;
#99552=CARTESIAN_POINT ( 'NONE',  ( -9.842984802582158466, 253.5906959047565294, 1.781981959250518832 ) ) ;
#99599=DIRECTION ( 'NONE',  ( 0.000000000000000000, 0.000000000000000000, -1.000000000000000000 ) ) ;
#99608=EDGE_LOOP ( 'NONE', ( #35000, #92167 ) ) ;
#99660=CARTESIAN_POINT ( 'NONE',  ( 5.650483388624518710, -81.54433403149616311, 2.031129859422142303 ) ) ;
#99848=CARTESIAN_POINT ( 'NONE',  ( 7.046289519167717508, -83.69408180055621926, -3.789821819998814512 ) ) ;
#99944=CARTESIAN_POINT ( 'NONE',  ( -7.412906595240167817, -12.64188272852255324, 3.014362223629234894 ) ) ;
#100002=DIRECTION ( 'NONE',  ( -0.000000000000000000, 1.000000000000000000, -0.000000000000000000 ) ) ;
#100081=FACE_OUTER_BOUND ( 'NONE', #24628, .T. ) ;
#100105=ADVANCED_FACE ( 'NONE', ( #46643, #64952 ), #31555, .T. ) ;
#100143=AXIS2_PLACEMENT_3D ( 'NONE', #29205, #97574, #16679 ) ;
#100144=CARTESIAN_POINT ( 'NONE',  ( 5.092539576892244568, -12.44323467208434053, 3.177249149099051984 ) ) ;
#100156=CARTESIAN_POINT ( 'NONE',  ( -5.477432325710314132, 246.8352046442952030, 2.459915882346695337 ) ) ;
#100188=CARTESIAN_POINT ( 'NONE',  ( -9.380894568449098969, 247.9886936688905337, -3.467341429141166387 ) ) ;
#100194=CARTESIAN_POINT ( 'NONE',  ( 5.190609988845227285, -82.36077713256410959, -3.016375611400009316 ) ) ;
#100246=CARTESIAN_POINT ( 'NONE',  ( 5.981118819178460555, 246.0281654381993803, 0.5452870891823716759 ) ) ;
#100249=( GEOMETRIC_REPRESENTATION_CONTEXT ( 3 ) GLOBAL_UNCERTAINTY_ASSIGNED_CONTEXT ( ( #93096 ) ) GLOBAL_UNIT_ASSIGNED_CONTEXT ( ( #4142, #94761, #68890 ) ) REPRESENTATION_CONTEXT ( 'NONE', 'WORKASPACE' ) );
#100354=CARTESIAN_POINT ( 'NONE',  ( -7.801642220026311136, -61.41203173850968966, 1.787233835843584417 ) ) ;
#100506=DIRECTION ( 'NONE',  ( 0.000000000000000000, 0.000000000000000000, -1.000000000000000000 ) ) ;
#100530=CARTESIAN_POINT ( 'NONE',  ( 6.928203230275508773, -10.00000000000001066, -4.000000000000000000 ) ) ;
#100573=ADVANCED_FACE ( 'NONE', ( #87522 ), #70798, .F. ) ;
#100621=CARTESIAN_POINT ( 'NONE',  ( 4.903871675326597845, 252.0208580730149492, -3.461400506969868118 ) ) ;
#100638=ORIENTED_EDGE ( 'NONE', *, *, #48782, .F. ) ;
#100672=CARTESIAN_POINT ( 'NONE',  ( 5.856955515201468288, -13.78289058880865525, 1.326217528971456838 ) ) ;
#100681=CARTESIAN_POINT ( 'NONE',  ( -4.521127550501226722, 249.3238975947233200, 3.944701057164360147 ) ) ;
#100715=CARTESIAN_POINT ( 'NONE',  ( -9.989285784994832440, 246.0265757255429264, 0.5301777604595956372 ) ) ;
#100856=CARTESIAN_POINT ( 'NONE',  ( 9.698972129396524977, 253.1762971274193887, -2.445345647270337430 ) ) ;
#100883=CARTESIAN_POINT ( 'NONE',  ( 7.551560007654696705, -13.00910351806993148, -2.648022159607832826 ) ) ;
#100905=DIRECTION ( 'NONE',  ( -1.000000000000000000, 0.000000000000000000, 0.000000000000000000 ) ) ;
#100922=EDGE_CURVE ( 'NONE', #73080, #92577, #50433, .T. ) ;
#100966=CARTESIAN_POINT ( 'NONE',  ( -4.589925132946517827, 251.0652601629250285, 3.864926970398266270 ) ) ;
#101031=CARTESIAN_POINT ( 'NONE',  ( -4.656390720430125363, -8.683538140394544413, 3.786082374785830762 ) ) ;
#101065=AXIS2_PLACEMENT_3D ( 'NONE', #88101, #77354, #86001 ) ;
#101104=( LENGTH_UNIT ( ) NAMED_UNIT ( * ) SI_UNIT ( .MILLI., .METRE. ) );
#101197=CARTESIAN_POINT ( 'NONE',  ( 7.344505440741523117, -62.55381072701295153, -3.175463080953004447 ) ) ;
#101242=CARTESIAN_POINT ( 'NONE',  ( 7.744168461338430731, -88.46254061715157491, 2.019395720771552050 ) ) ;
#101355=DIRECTION ( 'NONE',  ( 0.000000000000000000, 0.000000000000000000, 1.000000000000000000 ) ) ;
#101356=ADVANCED_BREP_SHAPE_REPRESENTATION ( '', ( #88119, #10728 ), #90114 ) ;
#101402=CARTESIAN_POINT ( 'NONE',  ( 9.165151389911702751, 250.2631950629487960, 4.000000000000000000 ) ) ;
#101433=CARTESIAN_POINT ( 'NONE',  ( 6.944371705245976578, -10.53899691424551222, -3.972324460300563409 ) ) ;
#101475=CIRCLE ( 'NONE', #8450, 1.000000000000000888 ) ;
#101483=ORIENTED_EDGE ( 'NONE', *, *, #233, .T. ) ;
#101571=CARTESIAN_POINT ( 'NONE',  ( -4.904566723942686224, -7.977572975292544832, 3.460360782932702328 ) ) ;
#101650=CARTESIAN_POINT ( 'NONE',  ( 9.177080501238327415, 249.4665305714572696, -3.972956046786645601 ) ) ;
#101657=DIRECTION ( 'NONE',  ( -0.000000000000000000, -1.000000000000000000, -0.000000000000000000 ) ) ;
#101696=CARTESIAN_POINT ( 'NONE',  ( 5.858881034796415754, 253.7858632400298404, 1.317748741875953034 ) ) ;
#101753=CARTESIAN_POINT ( 'NONE',  ( -4.478476647430157165, 249.7264792081795690, 3.992942460563209117 ) ) ;
#101762=CARTESIAN_POINT ( 'NONE',  ( 8.000113193197767814, -89.00022638645864959, -0.2613481123984638943 ) ) ;
#101785=CARTESIAN_POINT ( 'NONE',  ( 0.000000000000000000, -100.0000000000000000, 0.000000000000000000 ) ) ;
#101813=CARTESIAN_POINT ( 'NONE',  ( -7.744168461338432508, -6.537459382848431311, 2.019395720771551161 ) ) ;
#101817=VERTEX_POINT ( 'NONE', #39018 ) ;
#101843=CARTESIAN_POINT ( 'NONE',  ( 4.905018583967742707, 247.9764001432031364, -3.459768807258305490 ) ) ;
#101951=CARTESIAN_POINT ( 'NONE',  ( -4.813555570991610466, -66.79473796517321205, -3.584128953194789968 ) ) ;
#102001=CARTESIAN_POINT ( 'NONE',  ( -7.619701877737479201, -68.17442159532767221, -2.447562251315981374 ) ) ;
#102089=CARTESIAN_POINT ( 'NONE',  ( -5.092539576892243680, -7.556765327915675456, 3.177249149099054204 ) ) ;
#102152=B_SPLINE_CURVE_WITH_KNOTS ( 'NONE', 3,
 ( #55464, #392, #98591, #75380, #91588, #75919, #919, #25832, #100194, #26359, #66772, #83475, #16083, #1479, #89979, #33899, #33359, #57586, #48963, #81861, #58136, #59220, #99660, #17170, #34443, #8519, #84014, #10120, #43030, #58686, #9574, #50557, #67313, #50041, #82951, #91062 ),
 .UNSPECIFIED., .F., .F.,
 ( 4, 2, 2, 2, 2, 2, 2, 2, 2, 2, 2, 2, 2, 2, 2, 2, 2, 4 ),
 ( 0.000000000000000000, 0.0008074604767267243646, 0.001614920953453448729, 0.002422381430180173094, 0.003229841906906897459, 0.004037302383633621823, 0.004844762860360346188, 0.005652223337087070552, 0.006459683813813794917, 0.007267144290540519282, 0.008074604767267243646, 0.008882065243993968878, 0.009689525720720692376, 0.01049698619744741587, 0.01130444667417414110, 0.01211190715090086634, 0.01251563738926422809, 0.01291936762762758983 ),
 .UNSPECIFIED. ) ;
#102164=CARTESIAN_POINT ( 'NONE',  ( -4.478476647430159829, -10.27352079182045941, 3.992942460563206009 ) ) ;
#102262=CARTESIAN_POINT ( 'NONE',  ( -4.595881407952572495, -83.93374566798678416, -3.857520671226066789 ) ) ;
#102274=CARTESIAN_POINT ( 'NONE',  ( -7.212408192734265810, -87.01517089320367404, -3.465038817813880456 ) ) ;
#102276=ORIENTED_EDGE ( 'NONE', *, *, #79589, .T. ) ;
#102287=ORIENTED_EDGE ( 'NONE', *, *, #77181, .T. ) ;
#102361=CARTESIAN_POINT ( 'NONE',  ( 7.934996450857313199, -68.86862456472532301, -1.050865690281774123 ) ) ;
#102375=CARTESIAN_POINT ( 'NONE',  ( 5.855777637195783925, -6.218935032415544129, -1.331220292256673154 ) ) ;
#102386=ADVANCED_FACE ( 'NONE', ( #37815 ), #75657, .T. ) ;
#102463=CARTESIAN_POINT ( 'NONE',  ( 9.842473135306434529, 253.5893181711358295, 1.785129593756250355 ) ) ;
#102496=CARTESIAN_POINT ( 'NONE',  ( -4.472135954999577834, -65.27411850998326770, -4.000000000000002665 ) ) ;
#102596=VERTEX_POINT ( 'NONE', #53585 ) ;
#102633=CARTESIAN_POINT ( 'NONE',  ( -5.646888413699862497, -6.550258440296117257, 2.040714635159913470 ) ) ;
#102701=CARTESIAN_POINT ( 'NONE',  ( -5.982126593009819970, -13.97334227892932290, 0.5333292889181908691 ) ) ;
#102723=EDGE_CURVE ( 'NONE', #89178, #78936, #26690, .T. ) ;
#102751=DIRECTION ( 'NONE',  ( 1.000000000000000000, -0.000000000000000000, -0.000000000000000000 ) ) ;
#102759=CARTESIAN_POINT ( 'NONE',  ( 4.497431761510343406, 250.5409812425103837, -3.972160586670077542 ) ) ;
#102794=CARTESIAN_POINT ( 'NONE',  ( 6.943482370013978944, -64.47151629739275336, 3.973876482044369940 ) ) ;
#102801=CARTESIAN_POINT ( 'NONE',  ( -5.858824175751784047, -81.21420939127644090, -1.318356988357131998 ) ) ;
#102814=CARTESIAN_POINT ( 'NONE',  ( -7.743982712349851916, -88.46213014760735405, 2.020119794285909709 ) ) ;
#102821=CARTESIAN_POINT ( 'NONE',  ( -4.660674839411964143, -63.68217514695592740, -3.778981567323764335 ) ) ;
#102835=SURFACE_STYLE_FILL_AREA ( #20909 ) ;
#102837=DIRECTION ( 'NONE',  ( 0.000000000000000000, -1.000000000000000000, -0.000000000000000000 ) ) ;
#102874=B_SPLINE_CURVE_WITH_KNOTS ( 'NONE', 3,
 ( #69865, #34867, #102759, #20838, #10020, #18683, #100621, #84453, #69344, #44533, #42927, #35400, #92528, #51539, #28372, #68813, #43464, #26783, #43989, #59652, #101696, #76340, #2453, #68268, #27323, #93072, #19238, #76876, #85524, #11602, #14255, #79534, #80056, #30482, #13193, #54710 ),
 .UNSPECIFIED., .F., .F.,
 ( 4, 2, 2, 2, 2, 2, 2, 2, 2, 2, 2, 2, 2, 2, 2, 2, 2, 4 ),
 ( 2.830577590387642528E-17, 0.0008074604767267502771, 0.001614920953453472799, 0.002422381430180194778, 0.003229841906906917408, 0.004037302383633640038, 0.004844762860360361800, 0.005652223337087083563, 0.006459683813813806193, 0.007267144290540527955, 0.008074604767267248850, 0.008882065243993970613, 0.009689525720720692376, 0.01049698619744741414, 0.01130444667417413764, 0.01211190715090085940, 0.01251563738926421941, 0.01291936762762757943 ),
 .UNSPECIFIED. ) ;
#102886=DIRECTION ( 'NONE',  ( 1.000000000000000000, -0.000000000000000000, -0.000000000000000000 ) ) ;
#102913=CARTESIAN_POINT ( 'NONE',  ( 6.000469943554649355, -5.999295083295012709, 0.2622423038614494772 ) ) ;
#102996=CARTESIAN_POINT ( 'NONE',  ( 9.918010731619586906, 253.7915168484321384, -1.300854425901589950 ) ) ;
#103031=CARTESIAN_POINT ( 'NONE',  ( 7.551892080562057963, -13.00987702539385005, 2.647003822403974471 ) ) ;
#103049=( NAMED_UNIT ( * ) PLANE_ANGLE_UNIT ( ) SI_UNIT ( $, .RADIAN. ) );
#103050=FACE_OUTER_BOUND ( 'NONE', #50289, .T. ) ;
#103054=CARTESIAN_POINT ( 'NONE',  ( 6.928203230275508773, -85.00000000000000000, 4.000000000000001776 ) ) ;
#103080=CARTESIAN_POINT ( 'NONE',  ( -7.896165657598945842, -68.78911131371971521, -1.307894402814547830 ) ) ;
#103083=CARTESIAN_POINT ( 'NONE',  ( 0.000000000000000000, 3.000000000000002665, -13.00000000000003730 ) ) ;
#103148=CARTESIAN_POINT ( 'NONE',  ( 5.981118819178460555, -68.97183456180059125, 0.5452870891823740074 ) ) ;
#103345=CARTESIAN_POINT ( 'NONE',  ( -7.744991119775235688, -88.46438785425127094, -2.016316005557098112 ) ) ;
#103352=CARTESIAN_POINT ( 'NONE',  ( -6.000208918519489565, -60.99968662210032022, -0.2646532170642326709 ) ) ;
#103362=DIRECTION ( 'NONE',  ( 0.000000000000000000, 0.000000000000000000, -1.000000000000000000 ) ) ;
#103377=CARTESIAN_POINT ( 'NONE',  ( 7.618844049274133390, -6.827641010705410629, 2.450177051822844732 ) ) ;
#103412=CARTESIAN_POINT ( 'NONE',  ( -4.472135954999581386, -10.00000000000000888, -4.000000000000000000 ) ) ;
#103526=EDGE_CURVE ( 'NONE', #2575, #12726, #95454, .T. ) ;
#103566=FILL_AREA_STYLE ('',( #52351 ) ) ;
#103669=CARTESIAN_POINT ( 'NONE',  ( 5.909155701201247446, -68.86261680188732726, 1.073778020691679824 ) ) ;
#103760=CARTESIAN_POINT ( 'NONE',  ( -5.725004243152315375, -13.57519148255367547, -1.812899781754681472 ) ) ;
#103786=CYLINDRICAL_SURFACE ( 'NONE', #51106, 4.000000000000000000 ) ;
#103857=CARTESIAN_POINT ( 'NONE',  ( -7.550180524134850302, -88.00559247213188030, 2.651855549982492732 ) ) ;
#103899=MECHANICAL_DESIGN_GEOMETRIC_PRESENTATION_REPRESENTATION('',(#60811),#95295);
#104130=DIRECTION ( 'NONE',  ( 0.000000000000000000, 0.000000000000000000, -1.000000000000000000 ) ) ;
#104188=CARTESIAN_POINT ( 'NONE',  ( 4.813668318631093790, -66.79513229826685006, 3.583991016754781267 ) ) ;
#104211=VERTEX_POINT ( 'NONE', #84148 ) ;
#104243=CARTESIAN_POINT ( 'NONE',  ( 4.656390720430120034, -86.31646185960545381, 3.786082374785836535 ) ) ;
#104260=DIRECTION ( 'NONE',  ( 1.000000000000000000, -0.000000000000000000, -0.000000000000000000 ) ) ;
#104319=CARTESIAN_POINT ( 'NONE',  ( -7.414346147791996522, -12.64589157662264363, -3.010818766110527456 ) ) ;
#104346=AXIS2_PLACEMENT_3D ( 'NONE', #97845, #64438, #55253 ) ;
#104352=B_SPLINE_CURVE_WITH_KNOTS ( 'NONE', 3,
 ( #45017, #22344, #21285, #5069, #21812, #12084, #95671, #4007, #5593, #94633, #63320, #46065, #103760, #3481, #36420, #20777, #96215, #54120, #102701, #78948, #78415, #55190, #38516, #86548, #69804, #54652, #69291, #45542, #28864, #61191, #38003, #70338, #29897, #102164, #79481, #88117 ),
 .UNSPECIFIED., .F., .F.,
 ( 4, 2, 2, 2, 2, 2, 2, 2, 2, 2, 2, 2, 2, 2, 2, 2, 2, 4 ),
 ( 0.000000000000000000, 0.0008074604767267238225, 0.001614920953453447645, 0.002422381430180171359, 0.003229841906906895290, 0.004037302383633619221, 0.004844762860360342718, 0.005652223337087066216, 0.006459683813813790580, 0.007267144290540514077, 0.008074604767267238442, 0.008882065243993961939, 0.009689525720720685437, 0.01049698619744740893, 0.01130444667417413243, 0.01211190715090085593, 0.01251563738926422115, 0.01291936762762758636 ),
 .UNSPECIFIED. ) ;
#104429=CARTESIAN_POINT ( 'NONE',  ( -9.221249107921773103, 248.9517862850150891, 3.869340886054255968 ) ) ;
#104586=CARTESIAN_POINT ( 'NONE',  ( 9.165151389911699198, 249.9999999999999432, -4.000000000000002665 ) ) ;
#104602=B_SPLINE_CURVE_WITH_KNOTS ( 'NONE', 3,
 ( #4749, #43606, #3697, #60352, #93227, #77038, #76498, #45223, #35555, #85132, #69489, #44148, #20462, #102375, #28526, #61406, #53304, #102913, #86223, #78099, #4217, #37150, #79688, #89393, #39783, #64583, #71587, #7381, #97454, #96426, #30640, #106073, #72658, #23610, #56462, #54325 ),
 .UNSPECIFIED., .F., .F.,
 ( 4, 2, 2, 2, 2, 2, 2, 2, 2, 2, 2, 2, 2, 2, 2, 2, 2, 4 ),
 ( 0.000000000000000000, 0.0008074604767267249067, 0.001614920953453449813, 0.002422381430180174829, 0.003229841906906899627, 0.004037302383633624425, 0.004844762860360349657, 0.005652223337087074889, 0.006459683813813799254, 0.007267144290540524486, 0.008074604767267248850, 0.008882065243993974082, 0.009689525720720699314, 0.01049698619744742455, 0.01130444667417414978, 0.01211190715090087501, 0.01251563738926423329, 0.01291936762762759330 ),
 .UNSPECIFIED. ) ;
#104633=ORIENTED_EDGE ( 'NONE', *, *, #89448, .T. ) ;
#104634=ORIENTED_EDGE ( 'NONE', *, *, #66865, .T. ) ;
#104658=DIRECTION ( 'NONE',  ( 0.000000000000000000, 0.000000000000000000, -1.000000000000000000 ) ) ;
#104670=CARTESIAN_POINT ( 'NONE',  ( 4.472135954999578722, 249.9999999999999432, 4.000000000000002665 ) ) ;
#104699=CARTESIAN_POINT ( 'NONE',  ( -4.472135954999580498, -10.00000000000000888, 4.000000000000000000 ) ) ;
#104716=LINE ( 'NONE', #54556, #26844 ) ;
#104725=CARTESIAN_POINT ( 'NONE',  ( 6.000208918519489565, -69.00031337789968688, -0.2646532170642288406 ) ) ;
#104803=VERTEX_POINT ( 'NONE', #53644 ) ;
#104865=CARTESIAN_POINT ( 'NONE',  ( -7.002619243997879828, -11.05007318013818995, -3.868708944012998252 ) ) ;
#105333=CYLINDRICAL_SURFACE ( 'NONE', #63948, 4.000000000000000000 ) ;
#105422=CARTESIAN_POINT ( 'NONE',  ( 6.928203230275507885, -85.00000000000000000, -4.000000000000001776 ) ) ;
#105481=CARTESIAN_POINT ( 'NONE',  ( 9.537291425704623293, 247.3559562266722480, 3.012810007366010012 ) ) ;
#105485=CARTESIAN_POINT ( 'NONE',  ( 7.744991119775239241, -6.535612145748712187, -2.016316005557097668 ) ) ;
#105504=DIRECTION ( 'NONE',  ( 0.000000000000000000, 0.000000000000000000, 1.000000000000000000 ) ) ;
#105578=EDGE_LOOP ( 'NONE', ( #25160, #25648, #75847, #13862 ) ) ;
#105620=ORIENTED_EDGE ( 'NONE', *, *, #87798, .T. ) ;
#105649=CIRCLE ( 'NONE', #93586, 12.00000000000003908 ) ;
#105663=CARTESIAN_POINT ( 'NONE',  ( -5.728413875956868573, -68.58064226453402057, 1.802282772585249715 ) ) ;
#105731=CARTESIAN_POINT ( 'NONE',  ( 0.000000000000000000, -100.0000000000000000, -8.000000000000007105 ) ) ;
#105745=ADVANCED_FACE ( 'NONE', ( #100081 ), #26248, .F. ) ;
#105855=APPLICATION_CONTEXT ( 'automotive_design' ) ;
#105863=CARTESIAN_POINT ( 'NONE',  ( 7.344361273354515163, -87.44560530588523761, -3.175733139645588121 ) ) ;
#105996=CARTESIAN_POINT ( 'NONE',  ( 9.842984802582154913, 246.4093040952433853, 1.781981959250515946 ) ) ;
#106000=CARTESIAN_POINT ( 'NONE',  ( 6.928203230275510549, -10.00000000000000888, 4.000000000000000000 ) ) ;
#106034=CARTESIAN_POINT ( 'NONE',  ( -7.212994264445060644, -82.98288655659962387, 3.463766307298588032 ) ) ;
#106039=CARTESIAN_POINT ( 'NONE',  ( -9.948181520647874976, 253.8689280276036868, 1.049088206181511662 ) ) ;
#106061=PRODUCT_DEFINITION_CONTEXT ( 'detailed design', #74819, 'design' ) ;
#106070=CARTESIAN_POINT ( 'NONE',  ( -13.00000000000003730, -10.00000000000000888, 4.000000000000000000 ) ) ;
#106073=CARTESIAN_POINT ( 'NONE',  ( 4.521127550501230274, -9.323897594723373317, 3.944701057164355706 ) ) ;
#106074=CYLINDRICAL_SURFACE ( 'NONE', #64176, 6.000000000000000888 ) ;
#106104=AXIS2_PLACEMENT_3D ( 'NONE', #71317, #62716, #54583 ) ;
#106277=CARTESIAN_POINT ( 'NONE',  ( -4.590682673078522846, -86.06791757312156221, 3.864023243754608483 ) ) ;
#106326=COLOUR_RGB ( '', 0.09019608, 0.27058824, 0.51372549) ;
#106386=FACE_OUTER_BOUND ( 'NONE', #61675, .T. ) ;
#106428=VECTOR ( 'NONE', #97123, 1000.000000000000000 ) ;
#106435=CARTESIAN_POINT ( 'NONE',  ( -7.343637806710343163, -12.44363121900618729, 3.177475076494673534 ) ) ;
#106474=ADVANCED_FACE ( 'NONE', ( #56576, #48485, #16126, #64690, #39886 ), #8027, .F. ) ;
#106489=CARTESIAN_POINT ( 'NONE',  ( 0.000000000000000000, -100.0000000000000000, 0.000000000000000000 ) ) ;
#106493=DIRECTION ( 'NONE',  ( -0.000000000000000000, 1.000000000000000000, -0.000000000000000000 ) ) ;
#106576=CLOSED_SHELL ( 'NONE', ( #54019, #87346, #82390, #70720, #89137, #60828, #81516, #35992, #15052, #50574, #106474, #93156, #43767, #78831, #67436, #100105, #48239, #65303, #97874, #55371, #44737, #20263, #100573, #58517, #9895, #4465, #13484, #105745, #102386, #58495, #25899, #23149 ) ) ;
#106577=CARTESIAN_POINT ( 'NONE',  ( -7.934996450857311423, -81.13137543527469120, -1.050865690281774345 ) ) ;
#106583=CARTESIAN_POINT ( 'NONE',  ( -9.381593208289404018, 252.0143863811949529, -3.465401811657791598 ) ) ;
#106636=ORIENTED_EDGE ( 'NONE', *, *, #24617, .F. ) ;
#106690=CARTESIAN_POINT ( 'NONE',  ( 4.590682673078522846, -63.93208242687840936, 3.864023243754609371 ) ) ;
ENDSEC;
END-ISO-10303-21;
